ISO-10303-21;
HEADER;
/* Generated by software containing ST-Developer
 * from STEP Tools, Inc. (www.steptools.com) 
 */

FILE_DESCRIPTION(
/* description */ (''),
/* implementation_level */ '2;1');

FILE_NAME(
/* name */ 'Hex nut M4.step',
/* time_stamp */ '2026-11-15T17:46:57-08:00',
/* author */ (''),
/* organization */ (''),
/* preprocessor_version */ 'ST-DEVELOPER v20.2',
/* originating_system */ 'Autodesk Translation Framework v15.17.0.0',
/* authorisation */ '');

FILE_SCHEMA (('AUTOMOTIVE_DESIGN { 1 0 10303 214 3 1 1 }'));
ENDSEC;

DATA;
#10=MECHANICAL_DESIGN_GEOMETRIC_PRESENTATION_REPRESENTATION('',(#385),#12963);
#173=B_SPLINE_SURFACE_WITH_KNOTS('',3,3,((#12265,#12266,#12267,#12268,#12269,
#12270,#12271,#12272,#12273,#12274,#12275,#12276,#12277,#12278,#12279,#12280,
#12281,#12282,#12283,#12284,#12285,#12286,#12287,#12288,#12289,#12290,#12291,
#12292,#12293,#12294,#12295,#12296,#12297,#12298,#12299,#12300,#12301,#12302,
#12303,#12304,#12305),(#12306,#12307,#12308,#12309,#12310,#12311,#12312,
#12313,#12314,#12315,#12316,#12317,#12318,#12319,#12320,#12321,#12322,#12323,
#12324,#12325,#12326,#12327,#12328,#12329,#12330,#12331,#12332,#12333,#12334,
#12335,#12336,#12337,#12338,#12339,#12340,#12341,#12342,#12343,#12344,#12345,
#12346),(#12347,#12348,#12349,#12350,#12351,#12352,#12353,#12354,#12355,
#12356,#12357,#12358,#12359,#12360,#12361,#12362,#12363,#12364,#12365,#12366,
#12367,#12368,#12369,#12370,#12371,#12372,#12373,#12374,#12375,#12376,#12377,
#12378,#12379,#12380,#12381,#12382,#12383,#12384,#12385,#12386,#12387),
(#12388,#12389,#12390,#12391,#12392,#12393,#12394,#12395,#12396,#12397,
#12398,#12399,#12400,#12401,#12402,#12403,#12404,#12405,#12406,#12407,#12408,
#12409,#12410,#12411,#12412,#12413,#12414,#12415,#12416,#12417,#12418,#12419,
#12420,#12421,#12422,#12423,#12424,#12425,#12426,#12427,#12428)),
 .UNSPECIFIED.,.F.,.F.,.F.,(4,4),(4,1,1,1,1,1,1,1,1,1,1,1,1,1,1,1,1,1,1,
1,1,1,1,1,1,1,1,1,1,1,1,1,1,1,1,1,1,1,4),(0.,0.0448889834294934),(11.8615800042567,
12.8594360281068,13.8572920519568,14.8551480758068,15.8530040996568,16.8508601235068,
17.8487161473568,18.8465721712069,19.8444281950569,20.8422842189069,21.8401402427569,
22.8379962666069,23.8358522904569,24.833708314307,25.831564338157,26.829420362007,
27.827276385857,28.825132409707,29.822988433557,30.8208444574071,31.8187004812571,
32.8165565051071,33.8144125289571,34.8122685528071,35.8101245766571,36.8079806005072,
37.8058366243572,38.8036926482072,39.8015486720572,40.7994046959072,41.7972607197572,
42.7951167436073,43.7929727674573,44.7908287913073,45.7886848151573,46.7865408390073,
47.7843968628573,48.7822528867074,49.7801089105574),.UNSPECIFIED.);
#174=B_SPLINE_SURFACE_WITH_KNOTS('',3,3,((#12558,#12559,#12560,#12561,#12562,
#12563,#12564,#12565,#12566,#12567,#12568,#12569,#12570,#12571,#12572,#12573,
#12574,#12575,#12576,#12577,#12578,#12579,#12580,#12581,#12582,#12583,#12584,
#12585,#12586,#12587,#12588,#12589,#12590,#12591,#12592,#12593,#12594,#12595,
#12596,#12597,#12598),(#12599,#12600,#12601,#12602,#12603,#12604,#12605,
#12606,#12607,#12608,#12609,#12610,#12611,#12612,#12613,#12614,#12615,#12616,
#12617,#12618,#12619,#12620,#12621,#12622,#12623,#12624,#12625,#12626,#12627,
#12628,#12629,#12630,#12631,#12632,#12633,#12634,#12635,#12636,#12637,#12638,
#12639),(#12640,#12641,#12642,#12643,#12644,#12645,#12646,#12647,#12648,
#12649,#12650,#12651,#12652,#12653,#12654,#12655,#12656,#12657,#12658,#12659,
#12660,#12661,#12662,#12663,#12664,#12665,#12666,#12667,#12668,#12669,#12670,
#12671,#12672,#12673,#12674,#12675,#12676,#12677,#12678,#12679,#12680),
(#12681,#12682,#12683,#12684,#12685,#12686,#12687,#12688,#12689,#12690,
#12691,#12692,#12693,#12694,#12695,#12696,#12697,#12698,#12699,#12700,#12701,
#12702,#12703,#12704,#12705,#12706,#12707,#12708,#12709,#12710,#12711,#12712,
#12713,#12714,#12715,#12716,#12717,#12718,#12719,#12720,#12721)),
 .UNSPECIFIED.,.F.,.F.,.F.,(4,4),(4,1,1,1,1,1,1,1,1,1,1,1,1,1,1,1,1,1,1,
1,1,1,1,1,1,1,1,1,1,1,1,1,1,1,1,1,1,1,4),(0.,0.0448889834294934),(14.398141012777,
15.395997036627,16.393853060477,17.391709084327,18.389565108177,19.3874211320271,
20.3852771558771,21.3831331797271,22.3809892035771,23.3788452274271,24.3767012512771,
25.3745572751272,26.3724132989772,27.3702693228272,28.3681253466772,29.3659813705272,
30.3638373943772,31.3616934182273,32.3595494420773,33.3574054659273,34.3552614897773,
35.3531175136273,36.3509735374774,37.3488295613274,38.3466855851774,39.3445416090274,
40.3423976328774,41.3402536567274,42.3381096805775,43.3359657044275,44.3338217282775,
45.3316777521275,46.3295337759775,47.3273897998275,48.3252458236776,49.3231018475276,
50.3209578713776,51.3188138952276,52.3166699190776),.UNSPECIFIED.);
#320=B_SPLINE_CURVE_WITH_KNOTS('',3,(#11868,#11869,#11870,#11871),
 .UNSPECIFIED.,.F.,.F.,(4,4),(-35.9039160410262,-35.2623097995902),
 .UNSPECIFIED.);
#321=B_SPLINE_CURVE_WITH_KNOTS('',3,(#11877,#11878,#11879,#11880,#11881,
#11882,#11883,#11884,#11885,#11886,#11887,#11888,#11889,#11890,#11891,#11892,
#11893,#11894,#11895),.UNSPECIFIED.,.F.,.F.,(4,3,3,3,3,3,4),(32.7257487910699,
32.9292487870506,33.9271048109006,34.9249608347506,35.9228168586006,36.9206728824506,
37.9185289063006),.UNSPECIFIED.);
#322=B_SPLINE_CURVE_WITH_KNOTS('',3,(#11897,#11898,#11899,#11900,#11901,
#11902,#11903,#11904,#11905,#11906,#11907,#11908,#11909,#11910,#11911,#11912,
#11913,#11914,#11915,#11916,#11917,#11918),.UNSPECIFIED.,.F.,.F.,(4,3,3,
3,3,3,3,4),(-35.2623097995902,-34.9249608347506,-33.9271048109006,-32.9292487870506,
-31.9313927632006,-30.9335367393505,-29.9356807155005,-28.9791244924106),
 .UNSPECIFIED.);
#323=B_SPLINE_CURVE_WITH_KNOTS('',3,(#11923,#11924,#11925,#11926,#11927,
#11928,#11929,#11930,#11931,#11932,#11933,#11934,#11935,#11936,#11937,#11938,
#11939,#11940,#11941,#11942,#11943,#11944),.UNSPECIFIED.,.F.,.F.,(4,3,3,
3,3,3,3,4),(26.4425634838903,26.9421126439505,27.9399686678005,28.9378246916505,
29.9356807155005,30.9335367393505,31.9313927632005,32.7257487910699),
 .UNSPECIFIED.);
#324=B_SPLINE_CURVE_WITH_KNOTS('',3,(#11945,#11946,#11947,#11948,#11949,
#11950,#11951,#11952,#11953,#11954,#11955,#11956,#11957,#11958,#11959,#11960,
#11961,#11962,#11963,#11964,#11965,#11966,#11967,#11968,#11969),
 .UNSPECIFIED.,.F.,.F.,(4,3,3,3,3,3,3,3,4),(-28.9791244924106,-28.9378246916505,
-27.9399686678005,-26.9421126439505,-25.9442566201005,-24.9464005962504,
-23.9485445724004,-22.9506885485504,-22.695939185231),.UNSPECIFIED.);
#325=B_SPLINE_CURVE_WITH_KNOTS('',3,(#11974,#11975,#11976,#11977,#11978,
#11979,#11980,#11981,#11982,#11983,#11984,#11985,#11986,#11987,#11988,#11989,
#11990,#11991,#11992,#11993,#11994,#11995),.UNSPECIFIED.,.F.,.F.,(4,3,3,
3,3,3,3,4),(20.1593781767107,20.9549765008504,21.9528325247004,22.9506885485504,
23.9485445724004,24.9464005962504,25.9442566201004,26.4425634838903),
 .UNSPECIFIED.);
#326=B_SPLINE_CURVE_WITH_KNOTS('',3,(#11996,#11997,#11998,#11999,#12000,
#12001,#12002,#12003,#12004,#12005,#12006,#12007,#12008,#12009,#12010,#12011,
#12012,#12013,#12014,#12015,#12016,#12017),.UNSPECIFIED.,.F.,.F.,(4,3,3,
3,3,3,3,4),(-22.695939185231,-21.9528325247004,-20.9549765008504,-19.9571204770003,
-18.9592644531503,-17.9614084293003,-16.9635524054503,-16.4127538780514),
 .UNSPECIFIED.);
#327=B_SPLINE_CURVE_WITH_KNOTS('',3,(#12022,#12023,#12024,#12025,#12026,
#12027,#12028,#12029,#12030,#12031,#12032,#12033,#12034,#12035,#12036,#12037,
#12038,#12039,#12040,#12041,#12042,#12043,#12044,#12045,#12046),
 .UNSPECIFIED.,.F.,.F.,(4,3,3,3,3,3,3,3,4),(13.8761928695312,13.9699843339002,
14.9678403577503,15.9656963816003,16.9635524054503,17.9614084293003,18.9592644531503,
19.9571204770003,20.1593781767107),.UNSPECIFIED.);
#328=B_SPLINE_CURVE_WITH_KNOTS('',3,(#12047,#12048,#12049,#12050,#12051,
#12052,#12053,#12054,#12055,#12056,#12057,#12058,#12059,#12060,#12061,#12062,
#12063,#12064,#12065,#12066,#12067,#12068),.UNSPECIFIED.,.F.,.F.,(4,3,3,
3,3,3,3,4),(-16.4127538780514,-15.9656963816003,-14.9678403577503,-13.9699843339002,
-12.9721283100502,-11.9742722862002,-10.9764162623502,-10.1295685708718),
 .UNSPECIFIED.);
#329=B_SPLINE_CURVE_WITH_KNOTS('',3,(#12074,#12075,#12076,#12077,#12078,
#12079,#12080,#12081,#12082,#12083,#12084,#12085,#12086),.UNSPECIFIED.,
 .F.,.F.,(4,3,3,3,4),(-3.84638326369223,-2.99356807155005,-1.99571204770004,
-0.99785602385002,0.),.UNSPECIFIED.);
#330=B_SPLINE_CURVE_WITH_KNOTS('',3,(#12089,#12090,#12091,#12092,#12093,
#12094,#12095,#12096,#12097,#12098,#12099,#12100,#12101,#12102,#12103,#12104,
#12105,#12106,#12107),.UNSPECIFIED.,.F.,.F.,(4,3,3,3,3,3,4),(2.01461286527443,
2.99356807155005,3.99142409540007,4.98928011925009,5.9871361431001,6.98499216695013,
7.59300756235157),.UNSPECIFIED.);
#331=B_SPLINE_CURVE_WITH_KNOTS('',3,(#12113,#12114,#12115,#12116,#12117,
#12118),.UNSPECIFIED.,.F.,.F.,(4,1,1,4),(47.1238898038469,47.7843968628573,
48.7822528867074,49.7801089105574),.UNSPECIFIED.);
#332=B_SPLINE_CURVE_WITH_KNOTS('',3,(#12121,#12122,#12123,#12124,#12125,
#12126,#12127),.UNSPECIFIED.,.F.,.F.,(4,1,1,1,4),(47.1238898038469,47.3273897998275,
48.3252458236776,49.3231018475276,50.3020570538032),.UNSPECIFIED.);
#333=B_SPLINE_CURVE_WITH_KNOTS('',3,(#12132,#12133,#12134,#12135,#12136,
#12137,#12138,#12139,#12140,#12141),.UNSPECIFIED.,.F.,.F.,(4,1,1,1,1,1,
1,4),(40.8407044966673,41.7972607197572,42.7951167436073,43.7929727674573,
44.7908287913073,45.7886848151573,46.7865408390073,47.1238898038469),
 .UNSPECIFIED.);
#334=B_SPLINE_CURVE_WITH_KNOTS('',3,(#12142,#12143,#12144,#12145,#12146,
#12147,#12148,#12149,#12150,#12151),.UNSPECIFIED.,.F.,.F.,(4,1,1,1,1,1,
1,4),(40.8407044966673,41.3402536567274,42.3381096805775,43.3359657044275,
44.3338217282775,45.3316777521275,46.3295337759775,47.1238898038469),
 .UNSPECIFIED.);
#335=B_SPLINE_CURVE_WITH_KNOTS('',3,(#12156,#12157,#12158,#12159,#12160,
#12161,#12162,#12163,#12164,#12165,#12166),.UNSPECIFIED.,.F.,.F.,(4,1,1,
1,1,1,1,1,4),(34.5575191894877,34.8122685528071,35.8101245766571,36.8079806005072,
37.8058366243572,38.8036926482072,39.8015486720572,40.7994046959072,40.8407044966673),
 .UNSPECIFIED.);
#336=B_SPLINE_CURVE_WITH_KNOTS('',3,(#12167,#12168,#12169,#12170,#12171,
#12172,#12173,#12174,#12175,#12176),.UNSPECIFIED.,.F.,.F.,(4,1,1,1,1,1,
1,4),(34.5575191894877,35.3531175136273,36.3509735374774,37.3488295613274,
38.3466855851774,39.3445416090274,40.3423976328774,40.8407044966673),
 .UNSPECIFIED.);
#337=B_SPLINE_CURVE_WITH_KNOTS('',3,(#12181,#12182,#12183,#12184,#12185,
#12186,#12187,#12188,#12189,#12190),.UNSPECIFIED.,.F.,.F.,(4,1,1,1,1,1,
1,4),(28.2743338823081,28.825132409707,29.822988433557,30.8208444574071,
31.8187004812571,32.8165565051071,33.8144125289571,34.5575191894877),
 .UNSPECIFIED.);
#338=B_SPLINE_CURVE_WITH_KNOTS('',3,(#12191,#12192,#12193,#12194,#12195,
#12196,#12197,#12198,#12199,#12200,#12201),.UNSPECIFIED.,.F.,.F.,(4,1,1,
1,1,1,1,1,4),(28.2743338823081,28.3681253466772,29.3659813705272,30.3638373943772,
31.3616934182273,32.3595494420773,33.3574054659273,34.3552614897773,34.5575191894877),
 .UNSPECIFIED.);
#339=B_SPLINE_CURVE_WITH_KNOTS('',3,(#12206,#12207,#12208,#12209,#12210,
#12211,#12212,#12213,#12214,#12215),.UNSPECIFIED.,.F.,.F.,(4,1,1,1,1,1,
1,4),(21.9911485751285,22.8379962666069,23.8358522904569,24.833708314307,
25.831564338157,26.829420362007,27.827276385857,28.2743338823081),
 .UNSPECIFIED.);
#340=B_SPLINE_CURVE_WITH_KNOTS('',3,(#12216,#12217,#12218,#12219,#12220,
#12221,#12222,#12223,#12224,#12225),.UNSPECIFIED.,.F.,.F.,(4,1,1,1,1,1,
1,4),(21.9911485751285,22.3809892035771,23.3788452274271,24.3767012512771,
25.3745572751272,26.3724132989772,27.3702693228272,28.2743338823081),
 .UNSPECIFIED.);
#341=B_SPLINE_CURVE_WITH_KNOTS('',3,(#12231,#12232,#12233,#12234,#12235),
 .UNSPECIFIED.,.F.,.F.,(4,1,4),(14.398141012777,15.395997036627,15.7079632679489),
 .UNSPECIFIED.);
#342=B_SPLINE_CURVE_WITH_KNOTS('',3,(#12238,#12239,#12240,#12241,#12242),
 .UNSPECIFIED.,.F.,.F.,(4,1,4),(13.8761928695312,14.8551480758068,15.7079632679489),
 .UNSPECIFIED.);
#343=B_SPLINE_CURVE_WITH_KNOTS('',3,(#12244,#12245,#12246,#12247,#12248,
#12249,#12250,#12251,#12252,#12253,#12254),.UNSPECIFIED.,.F.,.F.,(4,1,1,
1,1,1,1,1,4),(15.7079632679489,15.8530040996568,16.8508601235068,17.8487161473568,
18.8465721712069,19.8444281950569,20.8422842189069,21.8401402427569,21.9911485751285),
 .UNSPECIFIED.);
#344=B_SPLINE_CURVE_WITH_KNOTS('',3,(#12255,#12256,#12257,#12258,#12259,
#12260,#12261,#12262,#12263,#12264),.UNSPECIFIED.,.F.,.F.,(4,1,1,1,1,1,
1,4),(15.7079632679489,16.393853060477,17.391709084327,18.389565108177,
19.3874211320271,20.3852771558771,21.3831331797271,21.9911485751285),
 .UNSPECIFIED.);
#345=B_SPLINE_CURVE_WITH_KNOTS('',3,(#12429,#12430,#12431,#12432,#12433,
#12434,#12435,#12436,#12437,#12438,#12439,#12440,#12441,#12442,#12443,#12444,
#12445,#12446,#12447,#12448,#12449,#12450,#12451,#12452,#12453,#12454,#12455,
#12456,#12457,#12458,#12459,#12460,#12461,#12462,#12463,#12464,#12465,#12466,
#12467,#12468,#12469,#12470,#12471,#12472,#12473,#12474,#12475,#12476,#12477,
#12478,#12479,#12480),.UNSPECIFIED.,.F.,.F.,(4,3,3,3,3,3,3,3,3,3,3,3,3,
3,3,3,3,4),(0.,0.0396840521468864,0.059875020004076,0.0739768413530052,
0.0859734763696041,0.12472674289153,0.15053968360953,0.161721130091714,
0.197217246712606,0.224559338868372,0.235244538191998,0.270292231220177,
0.290140832661352,0.305406213186563,0.333032234601024,0.347218928912509,
0.375435310304714,0.378621596831395),.UNSPECIFIED.);
#346=B_SPLINE_CURVE_WITH_KNOTS('',3,(#12481,#12482,#12483,#12484,#12485,
#12486,#12487,#12488,#12489,#12490,#12491,#12492,#12493,#12494,#12495,#12496,
#12497,#12498,#12499,#12500,#12501,#12502,#12503,#12504,#12505,#12506,#12507,
#12508,#12509,#12510,#12511,#12512,#12513,#12514,#12515,#12516,#12517,#12518,
#12519,#12520,#12521,#12522,#12523,#12524,#12525,#12526,#12527,#12528,#12529,
#12530,#12531,#12532),.UNSPECIFIED.,.F.,.F.,(4,3,3,3,3,3,3,3,3,3,3,3,3,
3,3,3,3,4),(0.,0.0336993562019562,0.0587206748846584,0.0734845893515782,
0.10979434417143,0.132864732420192,0.14363295898452,0.177258566323581,0.196035872055507,
0.207661896409673,0.24493922230234,0.26977275930509,0.282653420233469,0.310317023711199,
0.326845507637221,0.342480201732081,0.373057649428629,0.376940817211641),
 .UNSPECIFIED.);
#347=B_SPLINE_CURVE_WITH_KNOTS('',3,(#12533,#12534,#12535,#12536,#12537,
#12538,#12539,#12540,#12541,#12542,#12543,#12544,#12545,#12546,#12547,#12548,
#12549,#12550,#12551,#12552,#12553,#12554,#12555,#12556,#12557),
 .UNSPECIFIED.,.F.,.F.,(4,3,3,3,3,3,3,3,4),(-10.1295685708718,-9.97856023850017,
-8.98070421465016,-7.98284819080014,-6.98499216695012,-5.9871361431001,
-4.98928011925009,-3.99142409540007,-3.84638326369223),.UNSPECIFIED.);
#348=B_SPLINE_CURVE_WITH_KNOTS('',3,(#12722,#12723,#12724,#12725,#12726,
#12727,#12728,#12729,#12730,#12731,#12732,#12733,#12734,#12735,#12736,#12737,
#12738,#12739,#12740,#12741,#12742,#12743,#12744,#12745,#12746,#12747,#12748,
#12749,#12750,#12751,#12752,#12753,#12754,#12755,#12756,#12757,#12758,#12759,
#12760,#12761,#12762,#12763,#12764,#12765,#12766,#12767,#12768,#12769,#12770,
#12771,#12772,#12773),.UNSPECIFIED.,.F.,.F.,(4,3,3,3,3,3,3,3,3,3,3,3,3,
3,3,3,3,4),(0.,0.0336994181656691,0.058720699944575,0.0734845927808491,
0.109794365269302,0.132864771817205,0.143633027430854,0.177258566323583,
0.196035861323974,0.207661888854805,0.244939171913457,0.269772630388177,
0.282653282483456,0.310316825068278,0.326842481101116,0.3424799795213,0.373057649428634,
0.376940817211644),.UNSPECIFIED.);
#349=B_SPLINE_CURVE_WITH_KNOTS('',3,(#12774,#12775,#12776,#12777,#12778,
#12779,#12780,#12781,#12782,#12783,#12784,#12785,#12786,#12787,#12788,#12789,
#12790,#12791,#12792,#12793,#12794,#12795),.UNSPECIFIED.,.F.,.F.,(4,3,3,
3,3,3,3,4),(7.59300756235157,7.98284819080014,8.98070421465015,9.97856023850017,
10.9764162623502,11.9742722862002,12.9721283100502,13.8761928695312),
 .UNSPECIFIED.);
#350=B_SPLINE_CURVE_WITH_KNOTS('',3,(#12796,#12797,#12798,#12799,#12800,
#12801,#12802,#12803,#12804,#12805,#12806,#12807,#12808,#12809,#12810,#12811,
#12812,#12813,#12814,#12815,#12816,#12817,#12818,#12819,#12820,#12821,#12822,
#12823,#12824,#12825,#12826,#12827,#12828,#12829,#12830,#12831,#12832,#12833,
#12834,#12835,#12836,#12837,#12838,#12839,#12840,#12841,#12842,#12843,#12844,
#12845,#12846,#12847),.UNSPECIFIED.,.F.,.F.,(4,3,3,3,3,3,3,3,3,3,3,3,3,
3,3,3,3,4),(0.,0.0396840879963326,0.0598753046358157,0.0739780373014043,
0.0859735519163639,0.124726799518446,0.150539713843663,0.16172115065774,
0.19721724671262,0.224559319464973,0.235244508043305,0.270292208608664,
0.290140708581571,0.305406176565746,0.333032103859708,0.347218909613468,
0.37543531030474,0.378621596831421),.UNSPECIFIED.);
#361=SHAPE_REPRESENTATION_RELATIONSHIP('SRR','None',#13045,#373);
#373=ADVANCED_BREP_SHAPE_REPRESENTATION('',(#397),#12961);
#385=STYLED_ITEM('',(#13114),#397);
#397=MANIFOLD_SOLID_BREP('Body1',#4819);
#439=FACE_BOUND('',#1113,.T.);
#440=FACE_BOUND('',#1122,.T.);
#562=PLANE('',#5286);
#563=PLANE('',#5288);
#564=PLANE('',#5289);
#565=PLANE('',#5290);
#566=PLANE('',#5291);
#567=PLANE('',#5292);
#568=PLANE('',#5293);
#569=PLANE('',#5294);
#801=FACE_OUTER_BOUND('',#1097,.T.);
#802=FACE_OUTER_BOUND('',#1098,.T.);
#803=FACE_OUTER_BOUND('',#1099,.T.);
#804=FACE_OUTER_BOUND('',#1100,.T.);
#805=FACE_OUTER_BOUND('',#1101,.T.);
#806=FACE_OUTER_BOUND('',#1102,.T.);
#807=FACE_OUTER_BOUND('',#1103,.T.);
#808=FACE_OUTER_BOUND('',#1104,.T.);
#809=FACE_OUTER_BOUND('',#1105,.T.);
#810=FACE_OUTER_BOUND('',#1106,.T.);
#811=FACE_OUTER_BOUND('',#1107,.T.);
#812=FACE_OUTER_BOUND('',#1108,.T.);
#813=FACE_OUTER_BOUND('',#1109,.T.);
#814=FACE_OUTER_BOUND('',#1110,.T.);
#815=FACE_OUTER_BOUND('',#1111,.T.);
#816=FACE_OUTER_BOUND('',#1112,.T.);
#817=FACE_OUTER_BOUND('',#1114,.T.);
#818=FACE_OUTER_BOUND('',#1115,.T.);
#819=FACE_OUTER_BOUND('',#1116,.T.);
#820=FACE_OUTER_BOUND('',#1117,.T.);
#821=FACE_OUTER_BOUND('',#1118,.T.);
#822=FACE_OUTER_BOUND('',#1119,.T.);
#823=FACE_OUTER_BOUND('',#1120,.T.);
#824=FACE_OUTER_BOUND('',#1121,.T.);
#1097=EDGE_LOOP('',(#4294,#4295,#4296));
#1098=EDGE_LOOP('',(#4297,#4298,#4299,#4300,#4301));
#1099=EDGE_LOOP('',(#4302,#4303,#4304,#4305));
#1100=EDGE_LOOP('',(#4306,#4307,#4308,#4309));
#1101=EDGE_LOOP('',(#4310,#4311,#4312,#4313));
#1102=EDGE_LOOP('',(#4314,#4315,#4316,#4317));
#1103=EDGE_LOOP('',(#4318,#4319,#4320,#4321));
#1104=EDGE_LOOP('',(#4322,#4323,#4324,#4325));
#1105=EDGE_LOOP('',(#4326,#4327,#4328,#4329));
#1106=EDGE_LOOP('',(#4330,#4331,#4332,#4333));
#1107=EDGE_LOOP('',(#4334,#4335,#4336,#4337));
#1108=EDGE_LOOP('',(#4338,#4339,#4340,#4341));
#1109=EDGE_LOOP('',(#4342,#4343,#4344,#4345));
#1110=EDGE_LOOP('',(#4346,#4347,#4348,#4349,#4350,#4351,#4352,#4353,#4354,
#4355,#4356,#4357,#4358,#4359,#4360,#4361));
#1111=EDGE_LOOP('',(#4362,#4363,#4364,#4365,#4366,#4367,#4368,#4369,#4370,
#4371,#4372,#4373,#4374,#4375,#4376));
#1112=EDGE_LOOP('',(#4377,#4378,#4379,#4380,#4381,#4382));
#1113=EDGE_LOOP('',(#4383,#4384,#4385,#4386));
#1114=EDGE_LOOP('',(#4387,#4388,#4389,#4390));
#1115=EDGE_LOOP('',(#4391,#4392,#4393,#4394));
#1116=EDGE_LOOP('',(#4395,#4396,#4397,#4398));
#1117=EDGE_LOOP('',(#4399,#4400,#4401,#4402));
#1118=EDGE_LOOP('',(#4403,#4404,#4405,#4406));
#1119=EDGE_LOOP('',(#4407,#4408,#4409,#4410));
#1120=EDGE_LOOP('',(#4411,#4412,#4413,#4414));
#1121=EDGE_LOOP('',(#4415,#4416,#4417,#4418,#4419,#4420));
#1122=EDGE_LOOP('',(#4421,#4422,#4423,#4424,#4425));
#1497=LINE('',#11865,#1899);
#1498=LINE('',#11875,#1900);
#1499=LINE('',#11922,#1901);
#1500=LINE('',#11973,#1902);
#1501=LINE('',#12021,#1903);
#1502=LINE('',#12072,#1904);
#1503=LINE('',#12111,#1905);
#1504=LINE('',#12131,#1906);
#1505=LINE('',#12155,#1907);
#1506=LINE('',#12180,#1908);
#1507=LINE('',#12205,#1909);
#1508=LINE('',#12229,#1910);
#1509=LINE('',#12851,#1911);
#1510=LINE('',#12853,#1912);
#1511=LINE('',#12855,#1913);
#1512=LINE('',#12857,#1914);
#1513=LINE('',#12859,#1915);
#1514=LINE('',#12860,#1916);
#1515=LINE('',#12865,#1917);
#1516=LINE('',#12866,#1918);
#1517=LINE('',#12867,#1919);
#1518=LINE('',#12870,#1920);
#1519=LINE('',#12871,#1921);
#1520=LINE('',#12874,#1922);
#1521=LINE('',#12875,#1923);
#1522=LINE('',#12878,#1924);
#1523=LINE('',#12879,#1925);
#1524=LINE('',#12882,#1926);
#1525=LINE('',#12883,#1927);
#1526=LINE('',#12885,#1928);
#1899=VECTOR('',#6342,0.2);
#1900=VECTOR('',#6347,0.2);
#1901=VECTOR('',#6352,0.2);
#1902=VECTOR('',#6355,0.2);
#1903=VECTOR('',#6358,0.2);
#1904=VECTOR('',#6361,0.2);
#1905=VECTOR('',#6366,0.205475);
#1906=VECTOR('',#6371,0.205475);
#1907=VECTOR('',#6374,0.205475);
#1908=VECTOR('',#6377,0.205475);
#1909=VECTOR('',#6380,0.205475);
#1910=VECTOR('',#6383,0.205475);
#1911=VECTOR('',#6390,1.);
#1912=VECTOR('',#6391,1.);
#1913=VECTOR('',#6392,1.);
#1914=VECTOR('',#6393,1.);
#1915=VECTOR('',#6394,1.);
#1916=VECTOR('',#6395,1.);
#1917=VECTOR('',#6400,1.);
#1918=VECTOR('',#6401,1.);
#1919=VECTOR('',#6402,1.);
#1920=VECTOR('',#6405,1.);
#1921=VECTOR('',#6406,1.);
#1922=VECTOR('',#6409,1.);
#1923=VECTOR('',#6410,1.);
#1924=VECTOR('',#6413,1.);
#1925=VECTOR('',#6414,1.);
#1926=VECTOR('',#6417,1.);
#1927=VECTOR('',#6418,1.);
#1928=VECTOR('',#6421,1.);
#2005=CIRCLE('',#5269,0.1666);
#2006=CIRCLE('',#5271,0.1666);
#2007=CIRCLE('',#5276,0.1666);
#2008=CIRCLE('',#5278,0.205475);
#2009=CIRCLE('',#5284,0.205475);
#2406=VERTEX_POINT('',#11863);
#2407=VERTEX_POINT('',#11864);
#2408=VERTEX_POINT('',#11866);
#2409=VERTEX_POINT('',#11873);
#2410=VERTEX_POINT('',#11874);
#2411=VERTEX_POINT('',#11876);
#2412=VERTEX_POINT('',#11920);
#2413=VERTEX_POINT('',#11921);
#2414=VERTEX_POINT('',#11971);
#2415=VERTEX_POINT('',#11972);
#2416=VERTEX_POINT('',#12019);
#2417=VERTEX_POINT('',#12020);
#2418=VERTEX_POINT('',#12070);
#2419=VERTEX_POINT('',#12071);
#2420=VERTEX_POINT('',#12073);
#2421=VERTEX_POINT('',#12087);
#2422=VERTEX_POINT('',#12109);
#2423=VERTEX_POINT('',#12110);
#2424=VERTEX_POINT('',#12112);
#2425=VERTEX_POINT('',#12119);
#2426=VERTEX_POINT('',#12129);
#2427=VERTEX_POINT('',#12130);
#2428=VERTEX_POINT('',#12153);
#2429=VERTEX_POINT('',#12154);
#2430=VERTEX_POINT('',#12178);
#2431=VERTEX_POINT('',#12179);
#2432=VERTEX_POINT('',#12203);
#2433=VERTEX_POINT('',#12204);
#2434=VERTEX_POINT('',#12227);
#2435=VERTEX_POINT('',#12228);
#2436=VERTEX_POINT('',#12230);
#2437=VERTEX_POINT('',#12236);
#2438=VERTEX_POINT('',#12849);
#2439=VERTEX_POINT('',#12850);
#2440=VERTEX_POINT('',#12852);
#2441=VERTEX_POINT('',#12854);
#2442=VERTEX_POINT('',#12856);
#2443=VERTEX_POINT('',#12858);
#2444=VERTEX_POINT('',#12863);
#2445=VERTEX_POINT('',#12864);
#2446=VERTEX_POINT('',#12869);
#2447=VERTEX_POINT('',#12873);
#2448=VERTEX_POINT('',#12877);
#2449=VERTEX_POINT('',#12881);
#3043=EDGE_CURVE('',#2406,#2407,#1497,.T.);
#3044=EDGE_CURVE('',#2408,#2407,#2005,.F.);
#3045=EDGE_CURVE('',#2408,#2406,#320,.T.);
#3046=EDGE_CURVE('',#2409,#2410,#1498,.T.);
#3047=EDGE_CURVE('',#2410,#2411,#321,.T.);
#3048=EDGE_CURVE('',#2407,#2411,#2006,.F.);
#3049=EDGE_CURVE('',#2406,#2409,#322,.T.);
#3050=EDGE_CURVE('',#2412,#2413,#1499,.T.);
#3051=EDGE_CURVE('',#2413,#2410,#323,.T.);
#3052=EDGE_CURVE('',#2409,#2412,#324,.T.);
#3053=EDGE_CURVE('',#2414,#2415,#1500,.T.);
#3054=EDGE_CURVE('',#2415,#2413,#325,.T.);
#3055=EDGE_CURVE('',#2412,#2414,#326,.T.);
#3056=EDGE_CURVE('',#2416,#2417,#1501,.T.);
#3057=EDGE_CURVE('',#2417,#2415,#327,.T.);
#3058=EDGE_CURVE('',#2414,#2416,#328,.T.);
#3059=EDGE_CURVE('',#2418,#2419,#1502,.T.);
#3060=EDGE_CURVE('',#2418,#2420,#329,.T.);
#3061=EDGE_CURVE('',#2421,#2420,#2007,.T.);
#3062=EDGE_CURVE('',#2421,#2419,#330,.T.);
#3063=EDGE_CURVE('',#2422,#2423,#1503,.T.);
#3064=EDGE_CURVE('',#2423,#2424,#331,.T.);
#3065=EDGE_CURVE('',#2425,#2424,#2008,.T.);
#3066=EDGE_CURVE('',#2422,#2425,#332,.T.);
#3067=EDGE_CURVE('',#2426,#2427,#1504,.T.);
#3068=EDGE_CURVE('',#2427,#2423,#333,.T.);
#3069=EDGE_CURVE('',#2426,#2422,#334,.T.);
#3070=EDGE_CURVE('',#2428,#2429,#1505,.T.);
#3071=EDGE_CURVE('',#2429,#2427,#335,.T.);
#3072=EDGE_CURVE('',#2428,#2426,#336,.T.);
#3073=EDGE_CURVE('',#2430,#2431,#1506,.T.);
#3074=EDGE_CURVE('',#2431,#2429,#337,.T.);
#3075=EDGE_CURVE('',#2430,#2428,#338,.T.);
#3076=EDGE_CURVE('',#2432,#2433,#1507,.T.);
#3077=EDGE_CURVE('',#2433,#2431,#339,.T.);
#3078=EDGE_CURVE('',#2432,#2430,#340,.T.);
#3079=EDGE_CURVE('',#2434,#2435,#1508,.T.);
#3080=EDGE_CURVE('',#2436,#2434,#341,.T.);
#3081=EDGE_CURVE('',#2437,#2436,#2009,.T.);
#3082=EDGE_CURVE('',#2437,#2435,#342,.T.);
#3083=EDGE_CURVE('',#2435,#2433,#343,.T.);
#3084=EDGE_CURVE('',#2434,#2432,#344,.T.);
#3085=EDGE_CURVE('',#2424,#2408,#345,.T.);
#3086=EDGE_CURVE('',#2420,#2437,#346,.T.);
#3087=EDGE_CURVE('',#2416,#2418,#347,.T.);
#3088=EDGE_CURVE('',#2411,#2425,#348,.T.);
#3089=EDGE_CURVE('',#2419,#2417,#349,.T.);
#3090=EDGE_CURVE('',#2436,#2421,#350,.T.);
#3091=EDGE_CURVE('',#2438,#2439,#1509,.T.);
#3092=EDGE_CURVE('',#2439,#2440,#1510,.T.);
#3093=EDGE_CURVE('',#2440,#2441,#1511,.T.);
#3094=EDGE_CURVE('',#2441,#2442,#1512,.T.);
#3095=EDGE_CURVE('',#2442,#2443,#1513,.T.);
#3096=EDGE_CURVE('',#2443,#2438,#1514,.T.);
#3097=EDGE_CURVE('',#2444,#2445,#1515,.T.);
#3098=EDGE_CURVE('',#2445,#2438,#1516,.T.);
#3099=EDGE_CURVE('',#2444,#2443,#1517,.T.);
#3100=EDGE_CURVE('',#2446,#2444,#1518,.T.);
#3101=EDGE_CURVE('',#2446,#2442,#1519,.T.);
#3102=EDGE_CURVE('',#2447,#2446,#1520,.T.);
#3103=EDGE_CURVE('',#2447,#2441,#1521,.T.);
#3104=EDGE_CURVE('',#2448,#2447,#1522,.T.);
#3105=EDGE_CURVE('',#2448,#2440,#1523,.T.);
#3106=EDGE_CURVE('',#2449,#2448,#1524,.T.);
#3107=EDGE_CURVE('',#2449,#2439,#1525,.T.);
#3108=EDGE_CURVE('',#2445,#2449,#1526,.T.);
#4294=ORIENTED_EDGE('',*,*,#3043,.T.);
#4295=ORIENTED_EDGE('',*,*,#3044,.F.);
#4296=ORIENTED_EDGE('',*,*,#3045,.T.);
#4297=ORIENTED_EDGE('',*,*,#3046,.T.);
#4298=ORIENTED_EDGE('',*,*,#3047,.T.);
#4299=ORIENTED_EDGE('',*,*,#3048,.F.);
#4300=ORIENTED_EDGE('',*,*,#3043,.F.);
#4301=ORIENTED_EDGE('',*,*,#3049,.T.);
#4302=ORIENTED_EDGE('',*,*,#3050,.T.);
#4303=ORIENTED_EDGE('',*,*,#3051,.T.);
#4304=ORIENTED_EDGE('',*,*,#3046,.F.);
#4305=ORIENTED_EDGE('',*,*,#3052,.T.);
#4306=ORIENTED_EDGE('',*,*,#3053,.T.);
#4307=ORIENTED_EDGE('',*,*,#3054,.T.);
#4308=ORIENTED_EDGE('',*,*,#3050,.F.);
#4309=ORIENTED_EDGE('',*,*,#3055,.T.);
#4310=ORIENTED_EDGE('',*,*,#3056,.T.);
#4311=ORIENTED_EDGE('',*,*,#3057,.T.);
#4312=ORIENTED_EDGE('',*,*,#3053,.F.);
#4313=ORIENTED_EDGE('',*,*,#3058,.T.);
#4314=ORIENTED_EDGE('',*,*,#3059,.F.);
#4315=ORIENTED_EDGE('',*,*,#3060,.T.);
#4316=ORIENTED_EDGE('',*,*,#3061,.F.);
#4317=ORIENTED_EDGE('',*,*,#3062,.T.);
#4318=ORIENTED_EDGE('',*,*,#3063,.T.);
#4319=ORIENTED_EDGE('',*,*,#3064,.T.);
#4320=ORIENTED_EDGE('',*,*,#3065,.F.);
#4321=ORIENTED_EDGE('',*,*,#3066,.F.);
#4322=ORIENTED_EDGE('',*,*,#3067,.T.);
#4323=ORIENTED_EDGE('',*,*,#3068,.T.);
#4324=ORIENTED_EDGE('',*,*,#3063,.F.);
#4325=ORIENTED_EDGE('',*,*,#3069,.F.);
#4326=ORIENTED_EDGE('',*,*,#3070,.T.);
#4327=ORIENTED_EDGE('',*,*,#3071,.T.);
#4328=ORIENTED_EDGE('',*,*,#3067,.F.);
#4329=ORIENTED_EDGE('',*,*,#3072,.F.);
#4330=ORIENTED_EDGE('',*,*,#3073,.T.);
#4331=ORIENTED_EDGE('',*,*,#3074,.T.);
#4332=ORIENTED_EDGE('',*,*,#3070,.F.);
#4333=ORIENTED_EDGE('',*,*,#3075,.F.);
#4334=ORIENTED_EDGE('',*,*,#3076,.T.);
#4335=ORIENTED_EDGE('',*,*,#3077,.T.);
#4336=ORIENTED_EDGE('',*,*,#3073,.F.);
#4337=ORIENTED_EDGE('',*,*,#3078,.F.);
#4338=ORIENTED_EDGE('',*,*,#3079,.F.);
#4339=ORIENTED_EDGE('',*,*,#3080,.F.);
#4340=ORIENTED_EDGE('',*,*,#3081,.F.);
#4341=ORIENTED_EDGE('',*,*,#3082,.T.);
#4342=ORIENTED_EDGE('',*,*,#3079,.T.);
#4343=ORIENTED_EDGE('',*,*,#3083,.T.);
#4344=ORIENTED_EDGE('',*,*,#3076,.F.);
#4345=ORIENTED_EDGE('',*,*,#3084,.F.);
#4346=ORIENTED_EDGE('',*,*,#3085,.F.);
#4347=ORIENTED_EDGE('',*,*,#3064,.F.);
#4348=ORIENTED_EDGE('',*,*,#3068,.F.);
#4349=ORIENTED_EDGE('',*,*,#3071,.F.);
#4350=ORIENTED_EDGE('',*,*,#3074,.F.);
#4351=ORIENTED_EDGE('',*,*,#3077,.F.);
#4352=ORIENTED_EDGE('',*,*,#3083,.F.);
#4353=ORIENTED_EDGE('',*,*,#3082,.F.);
#4354=ORIENTED_EDGE('',*,*,#3086,.F.);
#4355=ORIENTED_EDGE('',*,*,#3060,.F.);
#4356=ORIENTED_EDGE('',*,*,#3087,.F.);
#4357=ORIENTED_EDGE('',*,*,#3058,.F.);
#4358=ORIENTED_EDGE('',*,*,#3055,.F.);
#4359=ORIENTED_EDGE('',*,*,#3052,.F.);
#4360=ORIENTED_EDGE('',*,*,#3049,.F.);
#4361=ORIENTED_EDGE('',*,*,#3045,.F.);
#4362=ORIENTED_EDGE('',*,*,#3088,.F.);
#4363=ORIENTED_EDGE('',*,*,#3047,.F.);
#4364=ORIENTED_EDGE('',*,*,#3051,.F.);
#4365=ORIENTED_EDGE('',*,*,#3054,.F.);
#4366=ORIENTED_EDGE('',*,*,#3057,.F.);
#4367=ORIENTED_EDGE('',*,*,#3089,.F.);
#4368=ORIENTED_EDGE('',*,*,#3062,.F.);
#4369=ORIENTED_EDGE('',*,*,#3090,.F.);
#4370=ORIENTED_EDGE('',*,*,#3080,.T.);
#4371=ORIENTED_EDGE('',*,*,#3084,.T.);
#4372=ORIENTED_EDGE('',*,*,#3078,.T.);
#4373=ORIENTED_EDGE('',*,*,#3075,.T.);
#4374=ORIENTED_EDGE('',*,*,#3072,.T.);
#4375=ORIENTED_EDGE('',*,*,#3069,.T.);
#4376=ORIENTED_EDGE('',*,*,#3066,.T.);
#4377=ORIENTED_EDGE('',*,*,#3091,.T.);
#4378=ORIENTED_EDGE('',*,*,#3092,.T.);
#4379=ORIENTED_EDGE('',*,*,#3093,.T.);
#4380=ORIENTED_EDGE('',*,*,#3094,.T.);
#4381=ORIENTED_EDGE('',*,*,#3095,.T.);
#4382=ORIENTED_EDGE('',*,*,#3096,.T.);
#4383=ORIENTED_EDGE('',*,*,#3086,.T.);
#4384=ORIENTED_EDGE('',*,*,#3081,.T.);
#4385=ORIENTED_EDGE('',*,*,#3090,.T.);
#4386=ORIENTED_EDGE('',*,*,#3061,.T.);
#4387=ORIENTED_EDGE('',*,*,#3059,.T.);
#4388=ORIENTED_EDGE('',*,*,#3089,.T.);
#4389=ORIENTED_EDGE('',*,*,#3056,.F.);
#4390=ORIENTED_EDGE('',*,*,#3087,.T.);
#4391=ORIENTED_EDGE('',*,*,#3097,.T.);
#4392=ORIENTED_EDGE('',*,*,#3098,.T.);
#4393=ORIENTED_EDGE('',*,*,#3096,.F.);
#4394=ORIENTED_EDGE('',*,*,#3099,.F.);
#4395=ORIENTED_EDGE('',*,*,#3100,.T.);
#4396=ORIENTED_EDGE('',*,*,#3099,.T.);
#4397=ORIENTED_EDGE('',*,*,#3095,.F.);
#4398=ORIENTED_EDGE('',*,*,#3101,.F.);
#4399=ORIENTED_EDGE('',*,*,#3102,.T.);
#4400=ORIENTED_EDGE('',*,*,#3101,.T.);
#4401=ORIENTED_EDGE('',*,*,#3094,.F.);
#4402=ORIENTED_EDGE('',*,*,#3103,.F.);
#4403=ORIENTED_EDGE('',*,*,#3104,.T.);
#4404=ORIENTED_EDGE('',*,*,#3103,.T.);
#4405=ORIENTED_EDGE('',*,*,#3093,.F.);
#4406=ORIENTED_EDGE('',*,*,#3105,.F.);
#4407=ORIENTED_EDGE('',*,*,#3106,.T.);
#4408=ORIENTED_EDGE('',*,*,#3105,.T.);
#4409=ORIENTED_EDGE('',*,*,#3092,.F.);
#4410=ORIENTED_EDGE('',*,*,#3107,.F.);
#4411=ORIENTED_EDGE('',*,*,#3108,.T.);
#4412=ORIENTED_EDGE('',*,*,#3107,.T.);
#4413=ORIENTED_EDGE('',*,*,#3091,.F.);
#4414=ORIENTED_EDGE('',*,*,#3098,.F.);
#4415=ORIENTED_EDGE('',*,*,#3108,.F.);
#4416=ORIENTED_EDGE('',*,*,#3097,.F.);
#4417=ORIENTED_EDGE('',*,*,#3100,.F.);
#4418=ORIENTED_EDGE('',*,*,#3102,.F.);
#4419=ORIENTED_EDGE('',*,*,#3104,.F.);
#4420=ORIENTED_EDGE('',*,*,#3106,.F.);
#4421=ORIENTED_EDGE('',*,*,#3085,.T.);
#4422=ORIENTED_EDGE('',*,*,#3044,.T.);
#4423=ORIENTED_EDGE('',*,*,#3048,.T.);
#4424=ORIENTED_EDGE('',*,*,#3088,.T.);
#4425=ORIENTED_EDGE('',*,*,#3065,.T.);
#4538=CYLINDRICAL_SURFACE('',#5268,0.1666);
#4539=CYLINDRICAL_SURFACE('',#5270,0.1666);
#4540=CYLINDRICAL_SURFACE('',#5272,0.1666);
#4541=CYLINDRICAL_SURFACE('',#5273,0.1666);
#4542=CYLINDRICAL_SURFACE('',#5274,0.1666);
#4543=CYLINDRICAL_SURFACE('',#5275,0.1666);
#4544=CYLINDRICAL_SURFACE('',#5277,0.205475);
#4545=CYLINDRICAL_SURFACE('',#5279,0.205475);
#4546=CYLINDRICAL_SURFACE('',#5280,0.205475);
#4547=CYLINDRICAL_SURFACE('',#5281,0.205475);
#4548=CYLINDRICAL_SURFACE('',#5282,0.205475);
#4549=CYLINDRICAL_SURFACE('',#5283,0.205475);
#4550=CYLINDRICAL_SURFACE('',#5285,0.205475);
#4551=CYLINDRICAL_SURFACE('',#5287,0.1666);
#4782=ADVANCED_FACE('',(#801),#4538,.F.);
#4783=ADVANCED_FACE('',(#802),#4539,.F.);
#4784=ADVANCED_FACE('',(#803),#4540,.F.);
#4785=ADVANCED_FACE('',(#804),#4541,.F.);
#4786=ADVANCED_FACE('',(#805),#4542,.F.);
#4787=ADVANCED_FACE('',(#806),#4543,.F.);
#4788=ADVANCED_FACE('',(#807),#4544,.F.);
#4789=ADVANCED_FACE('',(#808),#4545,.F.);
#4790=ADVANCED_FACE('',(#809),#4546,.F.);
#4791=ADVANCED_FACE('',(#810),#4547,.F.);
#4792=ADVANCED_FACE('',(#811),#4548,.F.);
#4793=ADVANCED_FACE('',(#812),#4549,.F.);
#4794=ADVANCED_FACE('',(#813),#4550,.F.);
#4795=ADVANCED_FACE('',(#814),#173,.F.);
#4796=ADVANCED_FACE('',(#815),#174,.F.);
#4797=ADVANCED_FACE('',(#816,#439),#562,.T.);
#4798=ADVANCED_FACE('',(#817),#4551,.F.);
#4799=ADVANCED_FACE('',(#818),#563,.T.);
#4800=ADVANCED_FACE('',(#819),#564,.T.);
#4801=ADVANCED_FACE('',(#820),#565,.T.);
#4802=ADVANCED_FACE('',(#821),#566,.T.);
#4803=ADVANCED_FACE('',(#822),#567,.T.);
#4804=ADVANCED_FACE('',(#823),#568,.T.);
#4805=ADVANCED_FACE('',(#824,#440),#569,.F.);
#4819=CLOSED_SHELL('',(#4782,#4783,#4784,#4785,#4786,#4787,#4788,#4789,
#4790,#4791,#4792,#4793,#4794,#4795,#4796,#4797,#4798,#4799,#4800,#4801,
#4802,#4803,#4804,#4805));
#5267=AXIS2_PLACEMENT_3D('',#11861,#6338,#6339);
#5268=AXIS2_PLACEMENT_3D('',#11862,#6340,#6341);
#5269=AXIS2_PLACEMENT_3D('',#11867,#6343,#6344);
#5270=AXIS2_PLACEMENT_3D('',#11872,#6345,#6346);
#5271=AXIS2_PLACEMENT_3D('',#11896,#6348,#6349);
#5272=AXIS2_PLACEMENT_3D('',#11919,#6350,#6351);
#5273=AXIS2_PLACEMENT_3D('',#11970,#6353,#6354);
#5274=AXIS2_PLACEMENT_3D('',#12018,#6356,#6357);
#5275=AXIS2_PLACEMENT_3D('',#12069,#6359,#6360);
#5276=AXIS2_PLACEMENT_3D('',#12088,#6362,#6363);
#5277=AXIS2_PLACEMENT_3D('',#12108,#6364,#6365);
#5278=AXIS2_PLACEMENT_3D('',#12120,#6367,#6368);
#5279=AXIS2_PLACEMENT_3D('',#12128,#6369,#6370);
#5280=AXIS2_PLACEMENT_3D('',#12152,#6372,#6373);
#5281=AXIS2_PLACEMENT_3D('',#12177,#6375,#6376);
#5282=AXIS2_PLACEMENT_3D('',#12202,#6378,#6379);
#5283=AXIS2_PLACEMENT_3D('',#12226,#6381,#6382);
#5284=AXIS2_PLACEMENT_3D('',#12237,#6384,#6385);
#5285=AXIS2_PLACEMENT_3D('',#12243,#6386,#6387);
#5286=AXIS2_PLACEMENT_3D('',#12848,#6388,#6389);
#5287=AXIS2_PLACEMENT_3D('',#12861,#6396,#6397);
#5288=AXIS2_PLACEMENT_3D('',#12862,#6398,#6399);
#5289=AXIS2_PLACEMENT_3D('',#12868,#6403,#6404);
#5290=AXIS2_PLACEMENT_3D('',#12872,#6407,#6408);
#5291=AXIS2_PLACEMENT_3D('',#12876,#6411,#6412);
#5292=AXIS2_PLACEMENT_3D('',#12880,#6415,#6416);
#5293=AXIS2_PLACEMENT_3D('',#12884,#6419,#6420);
#5294=AXIS2_PLACEMENT_3D('',#12886,#6422,#6423);
#6338=DIRECTION('axis',(0.,0.,1.));
#6339=DIRECTION('refdir',(1.,0.,0.));
#6340=DIRECTION('center_axis',(0.,0.,-1.));
#6341=DIRECTION('ref_axis',(-0.949090833458245,0.315002523554231,0.));
#6342=DIRECTION('',(0.,0.,-1.));
#6343=DIRECTION('center_axis',(0.,0.,-1.));
#6344=DIRECTION('ref_axis',(1.,0.,0.));
#6345=DIRECTION('center_axis',(0.,0.,-1.));
#6346=DIRECTION('ref_axis',(1.,0.,0.));
#6347=DIRECTION('',(0.,0.,-1.));
#6348=DIRECTION('center_axis',(0.,0.,-1.));
#6349=DIRECTION('ref_axis',(1.,0.,0.));
#6350=DIRECTION('center_axis',(0.,0.,-1.));
#6351=DIRECTION('ref_axis',(1.,0.,0.));
#6352=DIRECTION('',(0.,0.,-1.));
#6353=DIRECTION('center_axis',(0.,0.,-1.));
#6354=DIRECTION('ref_axis',(1.,0.,0.));
#6355=DIRECTION('',(0.,0.,-1.));
#6356=DIRECTION('center_axis',(0.,0.,-1.));
#6357=DIRECTION('ref_axis',(1.,0.,0.));
#6358=DIRECTION('',(0.,0.,-1.));
#6359=DIRECTION('center_axis',(0.,0.,-1.));
#6360=DIRECTION('ref_axis',(0.938432355146259,-0.345463044064985,0.));
#6361=DIRECTION('',(0.,0.,-1.));
#6362=DIRECTION('center_axis',(0.,0.,-1.));
#6363=DIRECTION('ref_axis',(1.,0.,0.));
#6364=DIRECTION('center_axis',(0.,0.,-1.));
#6365=DIRECTION('ref_axis',(0.0179423478205307,0.999839023120566,0.));
#6366=DIRECTION('',(1.22464679914735E-16,-6.20582083667111E-32,-1.));
#6367=DIRECTION('center_axis',(0.,0.,1.));
#6368=DIRECTION('ref_axis',(1.,-3.8427904741888E-16,0.));
#6369=DIRECTION('center_axis',(0.,0.,-1.));
#6370=DIRECTION('ref_axis',(1.,-3.8427904741888E-16,0.));
#6371=DIRECTION('',(1.22464679914735E-16,-6.20582083667111E-32,-1.));
#6372=DIRECTION('center_axis',(0.,0.,-1.));
#6373=DIRECTION('ref_axis',(1.,-3.8427904741888E-16,0.));
#6374=DIRECTION('',(1.22464679914735E-16,-6.20582083667111E-32,-1.));
#6375=DIRECTION('center_axis',(0.,0.,-1.));
#6376=DIRECTION('ref_axis',(1.,-3.8427904741888E-16,0.));
#6377=DIRECTION('',(1.22464679914735E-16,-6.20582083667111E-32,-1.));
#6378=DIRECTION('center_axis',(0.,0.,-1.));
#6379=DIRECTION('ref_axis',(1.,-3.8427904741888E-16,0.));
#6380=DIRECTION('',(1.22464679914735E-16,-6.20582083667111E-32,-1.));
#6381=DIRECTION('center_axis',(0.,0.,-1.));
#6382=DIRECTION('ref_axis',(-0.609355746674506,-0.79289695042594,0.));
#6383=DIRECTION('',(1.22464679914735E-16,-6.20582083667111E-32,-1.));
#6384=DIRECTION('center_axis',(0.,0.,-1.));
#6385=DIRECTION('ref_axis',(1.,-3.8427904741888E-16,0.));
#6386=DIRECTION('center_axis',(0.,0.,-1.));
#6387=DIRECTION('ref_axis',(1.,-3.8427904741888E-16,0.));
#6388=DIRECTION('center_axis',(0.,0.,1.));
#6389=DIRECTION('ref_axis',(1.,0.,0.));
#6390=DIRECTION('',(0.5,0.866025403784439,0.));
#6391=DIRECTION('',(-0.5,0.866025403784439,0.));
#6392=DIRECTION('',(-1.,1.37354477598826E-16,0.));
#6393=DIRECTION('',(-0.5,-0.866025403784439,0.));
#6394=DIRECTION('',(0.5,-0.866025403784439,0.));
#6395=DIRECTION('',(1.,-1.37354477598826E-16,0.));
#6396=DIRECTION('center_axis',(0.,0.,-1.));
#6397=DIRECTION('ref_axis',(1.,0.,0.));
#6398=DIRECTION('center_axis',(-1.37354477598826E-16,-1.,0.));
#6399=DIRECTION('ref_axis',(1.,-1.37354477598826E-16,0.));
#6400=DIRECTION('',(1.,-1.37354477598826E-16,0.));
#6401=DIRECTION('',(0.,0.,1.));
#6402=DIRECTION('',(0.,0.,1.));
#6403=DIRECTION('center_axis',(-0.866025403784439,-0.5,0.));
#6404=DIRECTION('ref_axis',(0.5,-0.866025403784439,0.));
#6405=DIRECTION('',(0.5,-0.866025403784439,0.));
#6406=DIRECTION('',(0.,0.,1.));
#6407=DIRECTION('center_axis',(-0.866025403784439,0.5,0.));
#6408=DIRECTION('ref_axis',(-0.5,-0.866025403784439,0.));
#6409=DIRECTION('',(-0.5,-0.866025403784439,0.));
#6410=DIRECTION('',(0.,0.,1.));
#6411=DIRECTION('center_axis',(1.37354477598826E-16,1.,0.));
#6412=DIRECTION('ref_axis',(-1.,1.37354477598826E-16,0.));
#6413=DIRECTION('',(-1.,1.37354477598826E-16,0.));
#6414=DIRECTION('',(0.,0.,1.));
#6415=DIRECTION('center_axis',(0.866025403784439,0.5,0.));
#6416=DIRECTION('ref_axis',(-0.5,0.866025403784439,0.));
#6417=DIRECTION('',(-0.5,0.866025403784439,0.));
#6418=DIRECTION('',(0.,0.,1.));
#6419=DIRECTION('center_axis',(0.866025403784439,-0.5,0.));
#6420=DIRECTION('ref_axis',(0.5,0.866025403784439,0.));
#6421=DIRECTION('',(0.5,0.866025403784439,0.));
#6422=DIRECTION('center_axis',(0.,0.,1.));
#6423=DIRECTION('ref_axis',(1.,0.,0.));
#11861=CARTESIAN_POINT('',(0.,0.,0.));
#11862=CARTESIAN_POINT('Origin',(0.,0.,0.2));
#11863=CARTESIAN_POINT('',(-0.166448982935848,-0.000123056367485261,0.00714803633902118));
#11864=CARTESIAN_POINT('',(-0.1666,2.04026156737949E-17,0.));
#11865=CARTESIAN_POINT('',(-0.1666,2.04026156737949E-17,0.2));
#11866=CARTESIAN_POINT('',(-0.133707694182663,0.0998962258211753,-3.72972504691399E-17));
#11867=CARTESIAN_POINT('Origin',(0.,0.,0.));
#11868=CARTESIAN_POINT('Ctrl Pts',(-0.13370774202371,0.0998962637199352,
-7.80625564189563E-17));
#11869=CARTESIAN_POINT('Ctrl Pts',(-0.154908007636265,0.0714511367790156,
0.00238267877967367));
#11870=CARTESIAN_POINT('Ctrl Pts',(-0.166218419498132,0.0355914785578886,
0.00476535755934742));
#11871=CARTESIAN_POINT('Ctrl Pts',(-0.166448982935848,-0.000123056367485261,
0.00714803633902118));
#11872=CARTESIAN_POINT('Origin',(0.,0.,0.2));
#11873=CARTESIAN_POINT('',(-0.166860410748999,-4.21553466717637E-5,0.0771480363390211));
#11874=CARTESIAN_POINT('',(-0.166654775959782,0.000146646548331295,0.0578519636609792));
#11875=CARTESIAN_POINT('',(-0.1666,2.04026156737949E-17,0.2));
#11876=CARTESIAN_POINT('',(-0.0769902040670466,-0.147743251885541,0.));
#11877=CARTESIAN_POINT('Ctrl Pts',(-0.166654775959782,0.000146646548331295,
0.0578519636609792));
#11878=CARTESIAN_POINT('Ctrl Pts',(-0.166758996638221,0.0114358133562754,
0.0570962429544575));
#11879=CARTESIAN_POINT('Ctrl Pts',(-0.165709525805481,0.0227058575110541,
0.0563405222479359));
#11880=CARTESIAN_POINT('Ctrl Pts',(-0.163435150898545,0.0337234259760408,
0.0555848015414142));
#11881=CARTESIAN_POINT('Ctrl Pts',(-0.15228282290737,0.0877477369249823,
0.0518791481053199));
#11882=CARTESIAN_POINT('Ctrl Pts',(-0.11167888524593,0.1357015190679,0.0481734946692255));
#11883=CARTESIAN_POINT('Ctrl Pts',(-0.0602476828221599,0.15561740130089,
0.0444678412331313));
#11884=CARTESIAN_POINT('Ctrl Pts',(-0.00881648039838925,0.175533283533879,
0.040762187797037));
#11885=CARTESIAN_POINT('Ctrl Pts',(0.053441986787712,0.16741126585694,0.0370565343609427));
#11886=CARTESIAN_POINT('Ctrl Pts',(0.0980813920646122,0.134988882613172,
0.0333508809248484));
#11887=CARTESIAN_POINT('Ctrl Pts',(0.142720797341511,0.102566499369405,
0.0296452274887542));
#11888=CARTESIAN_POINT('Ctrl Pts',(0.16974114070921,0.0458437505588112,
0.0259395740526599));
#11889=CARTESIAN_POINT('Ctrl Pts',(0.166648931992492,-0.00924353559174104,
0.0222339206165656));
#11890=CARTESIAN_POINT('Ctrl Pts',(0.163556723275773,-0.0643308217422941,
0.0185282671804714));
#11891=CARTESIAN_POINT('Ctrl Pts',(0.130351962474636,-0.117782645232805,
0.0148226137443772));
#11892=CARTESIAN_POINT('Ctrl Pts',(0.0825007717953625,-0.145037847677429,
0.0111169603082829));
#11893=CARTESIAN_POINT('Ctrl Pts',(0.0346495811160894,-0.172293050122053,
0.00741130687218866));
#11894=CARTESIAN_POINT('Ctrl Pts',(-0.0278480394413196,-0.17335163152079,
0.00370565343609431));
#11895=CARTESIAN_POINT('Ctrl Pts',(-0.0769902040670456,-0.147743251885542,
5.89805981832114E-17));
#11896=CARTESIAN_POINT('Origin',(0.,0.,0.));
#11897=CARTESIAN_POINT('Ctrl Pts',(-0.166448982935848,-0.000123056367485261,
0.00714803633902118));
#11898=CARTESIAN_POINT('Ctrl Pts',(-0.166570210461424,-0.018901335955032,
0.00840082062938137));
#11899=CARTESIAN_POINT('Ctrl Pts',(-0.163628378559591,-0.03763949574471,
0.00965360491974155));
#11900=CARTESIAN_POINT('Ctrl Pts',(-0.157450514586768,-0.0552386959973693,
0.0109063892101017));
#11901=CARTESIAN_POINT('Ctrl Pts',(-0.139176799762301,-0.107295971452211,
0.014612042646196));
#11902=CARTESIAN_POINT('Ctrl Pts',(-0.0925898286465717,-0.149388063444853,
0.0183176960822903));
#11903=CARTESIAN_POINT('Ctrl Pts',(-0.0389605451714495,-0.162261019033932,
0.0220233495183846));
#11904=CARTESIAN_POINT('Ctrl Pts',(0.0146687383036719,-0.175133974623011,
0.0257290029544788));
#11905=CARTESIAN_POINT('Ctrl Pts',(0.0753403341381858,-0.158787793808527,
0.029434656390573));
#11906=CARTESIAN_POINT('Ctrl Pts',(0.115241327743874,-0.120696966553578,
0.0331403098266672));
#11907=CARTESIAN_POINT('Ctrl Pts',(0.155142321349563,-0.0826061392986276,
0.0368459632627615));
#11908=CARTESIAN_POINT('Ctrl Pts',(0.174272712726426,-0.0227706656032114,
0.0405516166988558));
#11909=CARTESIAN_POINT('Ctrl Pts',(0.163889373105412,0.0314056858317542,
0.04425727013495));
#11910=CARTESIAN_POINT('Ctrl Pts',(0.153506033484398,0.0855820372667198,
0.0479629235710443));
#11911=CARTESIAN_POINT('Ctrl Pts',(0.113608962865507,0.134099266441235,
0.0516685770071386));
#11912=CARTESIAN_POINT('Ctrl Pts',(0.0624581433490313,0.154744419673635,
0.0553742304432329));
#11913=CARTESIAN_POINT('Ctrl Pts',(0.011307323832556,0.175389572906036,
0.0590798838793272));
#11914=CARTESIAN_POINT('Ctrl Pts',(-0.0510972445815037,0.168162650196322,
0.0627855373154215));
#11915=CARTESIAN_POINT('Ctrl Pts',(-0.0961762851695443,0.136371337065745,
0.0664911907515157));
#11916=CARTESIAN_POINT('Ctrl Pts',(-0.139389570227485,0.105895819868462,
0.0700434726140175));
#11917=CARTESIAN_POINT('Ctrl Pts',(-0.166681805131909,0.052847201533458,
0.0735957544765193));
#11918=CARTESIAN_POINT('Ctrl Pts',(-0.166860410748999,-4.21553466717637E-5,
0.0771480363390211));
#11919=CARTESIAN_POINT('Origin',(0.,0.,0.2));
#11920=CARTESIAN_POINT('',(-0.166562721528158,0.000151999276579301,0.147148036339021));
#11921=CARTESIAN_POINT('',(-0.166326519955886,-5.91534338763107E-7,0.127851963660979));
#11922=CARTESIAN_POINT('',(-0.1666,2.04026156737949E-17,0.2));
#11923=CARTESIAN_POINT('Ctrl Pts',(-0.166326519955886,-5.91534338763107E-7,
0.127851963660979));
#11924=CARTESIAN_POINT('Ctrl Pts',(-0.166325716020091,0.0278480319741386,
0.12599683023769));
#11925=CARTESIAN_POINT('Ctrl Pts',(-0.159710002166229,0.0556970392585184,
0.1241416968144));
#11926=CARTESIAN_POINT('Ctrl Pts',(-0.146481565318128,0.079937430264998,
0.122286563391111));
#11927=CARTESIAN_POINT('Ctrl Pts',(-0.120057588559947,0.128357930428352,
0.118580909955017));
#11928=CARTESIAN_POINT('Ctrl Pts',(-0.0672484579299266,0.16237983929433,
0.114875256518922));
#11929=CARTESIAN_POINT('Ctrl Pts',(-0.0122358634786086,0.166424502517241,
0.111169603082828));
#11930=CARTESIAN_POINT('Ctrl Pts',(0.0427767309727098,0.170469165740151,
0.107463949646734));
#11931=CARTESIAN_POINT('Ctrl Pts',(0.0999927892453255,0.144536583319994,
0.10375829621064));
#11932=CARTESIAN_POINT('Ctrl Pts',(0.133214635576823,0.100501528314839,
0.100052642774545));
#11933=CARTESIAN_POINT('Ctrl Pts',(0.16643648190832,0.0564664733096838,
0.096346989338451));
#11934=CARTESIAN_POINT('Ctrl Pts',(0.175664116298698,-0.00567105428046926,
0.0926413359023568));
#11935=CARTESIAN_POINT('Ctrl Pts',(0.156669843600291,-0.0574593209837368,
0.0889356824662625));
#11936=CARTESIAN_POINT('Ctrl Pts',(0.137675570901885,-0.109247587687005,
0.0852300290301683));
#11937=CARTESIAN_POINT('Ctrl Pts',(0.0904593911146922,-0.150686593503387,
0.0815243755940739));
#11938=CARTESIAN_POINT('Ctrl Pts',(0.0366459467445889,-0.162800257272089,
0.0778187221579796));
#11939=CARTESIAN_POINT('Ctrl Pts',(-0.0171674976255144,-0.17491392104079,
0.0741130687218853));
#11940=CARTESIAN_POINT('Ctrl Pts',(-0.0775782065785286,-0.157702242761811,
0.0704074152857911));
#11941=CARTESIAN_POINT('Ctrl Pts',(-0.11693320189458,-0.119048983744838,
0.0667017618496969));
#11942=CARTESIAN_POINT('Ctrl Pts',(-0.148262248379121,-0.0882785634005673,
0.0637518291201243));
#11943=CARTESIAN_POINT('Ctrl Pts',(-0.166247953720068,-0.0439202717840205,
0.0608018963905518));
#11944=CARTESIAN_POINT('Ctrl Pts',(-0.166654775959782,0.000146646548331295,
0.0578519636609792));
#11945=CARTESIAN_POINT('Ctrl Pts',(-0.166860410748999,-4.21553466717637E-5,
0.0771480363390211));
#11946=CARTESIAN_POINT('Ctrl Pts',(-0.166868122137229,-0.00232568019210335,
0.0773014079126136));
#11947=CARTESIAN_POINT('Ctrl Pts',(-0.166825290345314,-0.00460890815435789,
0.077454779486206));
#11948=CARTESIAN_POINT('Ctrl Pts',(-0.16673101454388,-0.00689000963011461,
0.0776081510597985));
#11949=CARTESIAN_POINT('Ctrl Pts',(-0.164453190568154,-0.0620043396439587,
0.0813138044958928));
#11950=CARTESIAN_POINT('Ctrl Pts',(-0.13214402985468,-0.115877296120208,
0.0850194579319871));
#11951=CARTESIAN_POINT('Ctrl Pts',(-0.0845964830895265,-0.143841137535084,
0.0887251113680814));
#11952=CARTESIAN_POINT('Ctrl Pts',(-0.0370489363243729,-0.17180497894996,
0.0924307648041757));
#11953=CARTESIAN_POINT('Ctrl Pts',(0.0257369964924607,-0.173859705303464,
0.0961364182402699));
#11954=CARTESIAN_POINT('Ctrl Pts',(0.0750113070876087,-0.149064254577995,
0.0998420716763641));
#11955=CARTESIAN_POINT('Ctrl Pts',(0.124285617682757,-0.124268803852526,
0.103547725112458));
#11956=CARTESIAN_POINT('Ctrl Pts',(0.160048306056219,-0.0726231760480842,
0.107253378548553));
#11957=CARTESIAN_POINT('Ctrl Pts',(0.165924163852847,-0.01777574960003,
0.110959031984647));
#11958=CARTESIAN_POINT('Ctrl Pts',(0.171800021649474,0.0370716768480245,
0.114664685420741));
#11959=CARTESIAN_POINT('Ctrl Pts',(0.147789048869266,0.0951209019396915,
0.118370338856835));
#11960=CARTESIAN_POINT('Ctrl Pts',(0.104885566869347,0.129791543346377,
0.12207599229293));
#11961=CARTESIAN_POINT('Ctrl Pts',(0.0619820848694269,0.164462184753062,
0.125781645729024));
#11962=CARTESIAN_POINT('Ctrl Pts',(0.000186093649795584,0.175754242474766,
0.129487299165118));
#11963=CARTESIAN_POINT('Ctrl Pts',(-0.052206247152358,0.158497110915842,
0.133192952601213));
#11964=CARTESIAN_POINT('Ctrl Pts',(-0.104598587954512,0.141239979356918,
0.136898606037307));
#11965=CARTESIAN_POINT('Ctrl Pts',(-0.147587278339187,0.0954336585173664,
0.140604259473401));
#11966=CARTESIAN_POINT('Ctrl Pts',(-0.161488067840993,0.0420526424254004,
0.144309912909495));
#11967=CARTESIAN_POINT('Ctrl Pts',(-0.165036893714247,0.0284246444600193,
0.145255954052671));
#11968=CARTESIAN_POINT('Ctrl Pts',(-0.16668987457928,0.0143029550371173,
0.146201995195846));
#11969=CARTESIAN_POINT('Ctrl Pts',(-0.166562721528158,0.000151999276579301,
0.147148036339021));
#11970=CARTESIAN_POINT('Origin',(0.,0.,0.2));
#11971=CARTESIAN_POINT('',(-0.166338651274879,-4.67853121875056E-5,0.217148036339021));
#11972=CARTESIAN_POINT('',(-0.166650872726138,-0.000148155484504217,0.197851963660979));
#11973=CARTESIAN_POINT('',(-0.1666,2.04026156737949E-17,0.2));
#11974=CARTESIAN_POINT('Ctrl Pts',(-0.166650872726138,-0.000148155484504217,
0.197851963660979));
#11975=CARTESIAN_POINT('Ctrl Pts',(-0.16624400073373,0.0439863598254954,
0.194897417520922));
#11976=CARTESIAN_POINT('Ctrl Pts',(-0.148202282970397,0.0884148461429154,
0.191942871380865));
#11977=CARTESIAN_POINT('Ctrl Pts',(-0.116787784478103,0.119194926752247,
0.188988325240808));
#11978=CARTESIAN_POINT('Ctrl Pts',(-0.0773870647862129,0.157799946293768,
0.185282671804713));
#11979=CARTESIAN_POINT('Ctrl Pts',(-0.0169500249703049,0.174935068326537,
0.181577018368619));
#11980=CARTESIAN_POINT('Ctrl Pts',(0.0368495126734258,0.162754204250394,
0.177871364932525));
#11981=CARTESIAN_POINT('Ctrl Pts',(0.0906490503171566,0.150573340174251,
0.174165711496431));
#11982=CARTESIAN_POINT('Ctrl Pts',(0.13781108578871,0.109076489989194,0.170460058060336));
#11983=CARTESIAN_POINT('Ctrl Pts',(0.156740392213101,0.0572648554840297,
0.166754404624242));
#11984=CARTESIAN_POINT('Ctrl Pts',(0.175669698637491,0.00545322097886432,
0.163048751188148));
#11985=CARTESIAN_POINT('Ctrl Pts',(0.166366276014719,-0.0566731978464093,
0.159343097752054));
#11986=CARTESIAN_POINT('Ctrl Pts',(0.133090063801353,-0.100667049200161,
0.155637444315959));
#11987=CARTESIAN_POINT('Ctrl Pts',(0.0998138515879878,-0.144660900553913,
0.151931790879865));
#11988=CARTESIAN_POINT('Ctrl Pts',(0.042564849784029,-0.170522184436142,
0.148226137443771));
#11989=CARTESIAN_POINT('Ctrl Pts',(-0.0124428237561262,-0.166409123794165,
0.144520484007676));
#11990=CARTESIAN_POINT('Ctrl Pts',(-0.0674504972962818,-0.162296063152188,
0.140814830571582));
#11991=CARTESIAN_POINT('Ctrl Pts',(-0.120216842572635,-0.128208657986004,
0.137109177135488));
#11992=CARTESIAN_POINT('Ctrl Pts',(-0.146580603767641,-0.0797554096725464,
0.133403523699394));
#11993=CARTESIAN_POINT('Ctrl Pts',(-0.159746073379281,-0.0555589468257773,
0.131553003686589));
#11994=CARTESIAN_POINT('Ctrl Pts',(-0.166327321892425,-0.0277799601148087,
0.129702483673784));
#11995=CARTESIAN_POINT('Ctrl Pts',(-0.166326519955886,-5.91534338763107E-7,
0.127851963660979));
#11996=CARTESIAN_POINT('Ctrl Pts',(-0.166562721528158,0.000151999276579301,
0.147148036339021));
#11997=CARTESIAN_POINT('Ctrl Pts',(-0.166191814696579,-0.0411264924201606,
0.14990764863194));
#11998=CARTESIAN_POINT('Ctrl Pts',(-0.150673833135845,-0.0826540099902898,
0.152667260924859));
#11999=CARTESIAN_POINT('Ctrl Pts',(-0.122880807906595,-0.112903193819225,
0.155426873217778));
#12000=CARTESIAN_POINT('Ctrl Pts',(-0.0855598698514573,-0.153522302627504,
0.159132526653873));
#12001=CARTESIAN_POINT('Ctrl Pts',(-0.026105105122248,-0.173804808899682,
0.162838180089967));
#12002=CARTESIAN_POINT('Ctrl Pts',(0.0282594425548545,-0.164463453749595,
0.166543833526061));
#12003=CARTESIAN_POINT('Ctrl Pts',(0.0826239902319573,-0.155122098599507,
0.170249486962155));
#12004=CARTESIAN_POINT('Ctrl Pts',(0.131898320856954,-0.116156882027153,
0.17395514039825));
#12005=CARTESIAN_POINT('Ctrl Pts',(0.153519979653527,-0.0654097770223532,
0.177660793834344));
#12006=CARTESIAN_POINT('Ctrl Pts',(0.1751416384501,-0.0146626720175531,
0.181366447270438));
#12007=CARTESIAN_POINT('Ctrl Pts',(0.169110625418251,0.0478663214196927,
0.185072100706532));
#12008=CARTESIAN_POINT('Ctrl Pts',(0.138188506492137,0.093545498793948,
0.188777754142626));
#12009=CARTESIAN_POINT('Ctrl Pts',(0.107266387566023,0.139224676168203,
0.192483407578721));
#12010=CARTESIAN_POINT('Ctrl Pts',(0.0514531627456449,0.168054037479467,
0.196189061014815));
#12011=CARTESIAN_POINT('Ctrl Pts',(-0.00369457792842184,0.166832770092881,
0.199894714450909));
#12012=CARTESIAN_POINT('Ctrl Pts',(-0.0588423186024886,0.165611502706295,
0.203600367887004));
#12013=CARTESIAN_POINT('Ctrl Pts',(-0.113324575130244,0.134339606621858,
0.207306021323098));
#12014=CARTESIAN_POINT('Ctrl Pts',(-0.142194204679298,0.0873363147171791,
0.211011674759192));
#12015=CARTESIAN_POINT('Ctrl Pts',(-0.15812971948515,0.0613913453576635,
0.213057128619135));
#12016=CARTESIAN_POINT('Ctrl Pts',(-0.166261474396152,0.0306532700081179,
0.215102582479078));
#12017=CARTESIAN_POINT('Ctrl Pts',(-0.166338651274879,-4.67853121875056E-5,
0.217148036339021));
#12018=CARTESIAN_POINT('Origin',(0.,0.,0.2));
#12019=CARTESIAN_POINT('',(-0.166734374774229,-0.000128818837332453,0.287148036339021));
#12020=CARTESIAN_POINT('',(-0.166813199754551,8.97901853038408E-5,0.267851963660979));
#12021=CARTESIAN_POINT('',(-0.1666,2.04026156737949E-17,0.2));
#12022=CARTESIAN_POINT('Ctrl Pts',(-0.166813199754551,8.97901853038408E-5,
0.267851963660979));
#12023=CARTESIAN_POINT('Ctrl Pts',(-0.166846982879129,0.00527956240150659,
0.267503658240248));
#12024=CARTESIAN_POINT('Ctrl Pts',(-0.166625794764039,0.0104664167280576,
0.267155352819518));
#12025=CARTESIAN_POINT('Ctrl Pts',(-0.166140220809639,0.0156284006424284,
0.266807047398787));
#12026=CARTESIAN_POINT('Ctrl Pts',(-0.16097415480692,0.070547222718839,
0.263101393962693));
#12027=CARTESIAN_POINT('Ctrl Pts',(-0.125882181662303,0.122650955880377,
0.259395740526599));
#12028=CARTESIAN_POINT('Ctrl Pts',(-0.0769327614968034,0.148081614095739,
0.255690087090505));
#12029=CARTESIAN_POINT('Ctrl Pts',(-0.027983341331303,0.173512272311101,
0.25198443365441));
#12030=CARTESIAN_POINT('Ctrl Pts',(0.0348235258550809,0.172269855580289,
0.248278780218316));
#12031=CARTESIAN_POINT('Ctrl Pts',(0.0827289131521439,0.144923236625853,
0.244573126782222));
#12032=CARTESIAN_POINT('Ctrl Pts',(0.130634300449207,0.117576617671417,
0.240867473346127));
#12033=CARTESIAN_POINT('Ctrl Pts',(0.163638207856949,0.064125796493358,
0.237161819910033));
#12034=CARTESIAN_POINT('Ctrl Pts',(0.166628309560831,0.00904564092131411,
0.233456166473939));
#12035=CARTESIAN_POINT('Ctrl Pts',(0.169618411264713,-0.0460345146507298,
0.229750513037845));
#12036=CARTESIAN_POINT('Ctrl Pts',(0.142594707264736,-0.102744004616759,
0.22604485960175));
#12037=CARTESIAN_POINT('Ctrl Pts',(0.0979312150883438,-0.135115852675218,
0.222339206165656));
#12038=CARTESIAN_POINT('Ctrl Pts',(0.0532677229119514,-0.167487700733677,
0.218633552729562));
#12039=CARTESIAN_POINT('Ctrl Pts',(-0.00903555744085632,-0.175521906884566,
0.214927899293468));
#12040=CARTESIAN_POINT('Ctrl Pts',(-0.0604502752026059,-0.155539645602405,
0.211222245857373));
#12041=CARTESIAN_POINT('Ctrl Pts',(-0.111864992964356,-0.135557384320243,
0.207516592421279));
#12042=CARTESIAN_POINT('Ctrl Pts',(-0.152391148135047,-0.0875586556050303,
0.203810938985185));
#12043=CARTESIAN_POINT('Ctrl Pts',(-0.163472025936457,-0.0335218327222879,
0.20010528554909));
#12044=CARTESIAN_POINT('Ctrl Pts',(-0.165718034179448,-0.0225689865854744,
0.199354178253053));
#12045=CARTESIAN_POINT('Ctrl Pts',(-0.166754308078833,-0.0113680704511269,
0.198603070957016));
#12046=CARTESIAN_POINT('Ctrl Pts',(-0.166650872726138,-0.000148155484504217,
0.197851963660979));
#12047=CARTESIAN_POINT('Ctrl Pts',(-0.166338651274879,-4.67853121875056E-5,
0.217148036339021));
#12048=CARTESIAN_POINT('Ctrl Pts',(-0.166401292150756,-0.0249645895358502,
0.218808235915172));
#12049=CARTESIAN_POINT('Ctrl Pts',(-0.16115772813329,-0.0498573468775544,
0.220468435491324));
#12050=CARTESIAN_POINT('Ctrl Pts',(-0.150473846254983,-0.0721418444426733,
0.222128635067475));
#12051=CARTESIAN_POINT('Ctrl Pts',(-0.126626855711259,-0.121882023972926,
0.225834288503569));
#12052=CARTESIAN_POINT('Ctrl Pts',(-0.0756758720534593,-0.158627695308512,
0.229539941939664));
#12053=CARTESIAN_POINT('Ctrl Pts',(-0.0209510900103489,-0.165553231974957,
0.233245595375758));
#12054=CARTESIAN_POINT('Ctrl Pts',(0.0337736920327618,-0.172478768641402,
0.236951248811852));
#12055=CARTESIAN_POINT('Ctrl Pts',(0.0922722724611822,-0.149584170638707,
0.240656902247946));
#12056=CARTESIAN_POINT('Ctrl Pts',(0.127758456442371,-0.107352704753372,
0.244362555684041));
#12057=CARTESIAN_POINT('Ctrl Pts',(0.16324464042356,-0.0651212388680367,
0.248068209120135));
#12058=CARTESIAN_POINT('Ctrl Pts',(0.175718427957517,-0.00355290510006166,
0.251773862556229));
#12059=CARTESIAN_POINT('Ctrl Pts',(0.159468129568603,0.0491603754423182,
0.255479515992324));
#12060=CARTESIAN_POINT('Ctrl Pts',(0.14321783117969,0.101873655984698,0.259185169428418));
#12061=CARTESIAN_POINT('Ctrl Pts',(0.0982434468679055,0.145731883301483,
0.262890822864512));
#12062=CARTESIAN_POINT('Ctrl Pts',(0.045138527575508,0.160652789432442,
0.266596476300606));
#12063=CARTESIAN_POINT('Ctrl Pts',(-0.00796639171688973,0.1755736955634,
0.2703021297367));
#12064=CARTESIAN_POINT('Ctrl Pts',(-0.0692018459899008,0.161557280508531,
0.274007783172795));
#12065=CARTESIAN_POINT('Ctrl Pts',(-0.110528459862841,0.125021229174222,
0.277713436608889));
#12066=CARTESIAN_POINT('Ctrl Pts',(-0.145601002111859,0.0940142802871293,
0.2808583031856));
#12067=CARTESIAN_POINT('Ctrl Pts',(-0.166334479996432,0.0467878777510125,
0.28400316976231));
#12068=CARTESIAN_POINT('Ctrl Pts',(-0.166734374774229,-0.000128818837332453,
0.287148036339021));
#12069=CARTESIAN_POINT('Origin',(0.,0.,0.2));
#12070=CARTESIAN_POINT('',(-0.166743774672904,0.000120896768023321,0.357148036339021));
#12071=CARTESIAN_POINT('',(-0.166378928688253,9.26016813348553E-5,0.337851963660979));
#12072=CARTESIAN_POINT('',(-0.1666,2.04026156737949E-17,0.2));
#12073=CARTESIAN_POINT('',(0.126907087985239,0.107935865304851,0.4));
#12074=CARTESIAN_POINT('Ctrl Pts',(-0.166743774672904,0.000120896768023321,
0.357148036339021));
#12075=CARTESIAN_POINT('Ctrl Pts',(-0.166347196302146,-0.0471069253752206,
0.360315063917731));
#12076=CARTESIAN_POINT('Ctrl Pts',(-0.14528367999841,-0.0946317549803691,
0.363482091496441));
#12077=CARTESIAN_POINT('Ctrl Pts',(-0.109779302776043,-0.125660187653584,
0.366649119075152));
#12078=CARTESIAN_POINT('Ctrl Pts',(-0.0682365898755026,-0.161965718721597,
0.370354772511246));
#12079=CARTESIAN_POINT('Ctrl Pts',(-0.00692331585482878,-0.175686514319717,
0.37406042594734));
#12080=CARTESIAN_POINT('Ctrl Pts',(0.0460947087719345,-0.160413783553521,
0.377766079383434));
#12081=CARTESIAN_POINT('Ctrl Pts',(0.0991127333986977,-0.145141052787325,
0.381471732819529));
#12082=CARTESIAN_POINT('Ctrl Pts',(0.143835508631551,-0.100874795656813,
0.385177386255623));
#12083=CARTESIAN_POINT('Ctrl Pts',(0.159759468393512,-0.0481584829850476,
0.388883039691717));
#12084=CARTESIAN_POINT('Ctrl Pts',(0.175683428155473,0.00455782968671844,
0.392588693127811));
#12085=CARTESIAN_POINT('Ctrl Pts',(0.162808572446542,0.0657241978997386,
0.396294346563906));
#12086=CARTESIAN_POINT('Ctrl Pts',(0.126907087985239,0.10793586530485,0.4));
#12087=CARTESIAN_POINT('',(-0.127144355350143,0.10812641955069,0.4));
#12088=CARTESIAN_POINT('Origin',(0.,0.,0.4));
#12089=CARTESIAN_POINT('Ctrl Pts',(-0.127144402274347,0.108126457236473,
0.4));
#12090=CARTESIAN_POINT('Ctrl Pts',(-0.0920292268904173,0.149320274449966,
0.396364536929966));
#12091=CARTESIAN_POINT('Ctrl Pts',(-0.0349623149552143,0.171908313823477,
0.392729073859932));
#12092=CARTESIAN_POINT('Ctrl Pts',(0.0188177088499946,0.165794607065857,
0.389093610789898));
#12093=CARTESIAN_POINT('Ctrl Pts',(0.0736360706839233,0.159562862163704,
0.385387957353804));
#12094=CARTESIAN_POINT('Ctrl Pts',(0.125039398382612,0.12351037530068,0.38168230391771));
#12095=CARTESIAN_POINT('Ctrl Pts',(0.149523239782922,0.074090212834763,
0.377976650481616));
#12096=CARTESIAN_POINT('Ctrl Pts',(0.174007081183232,0.0246700503688466,
0.374270997045521));
#12097=CARTESIAN_POINT('Ctrl Pts',(0.171571436285164,-0.0381177876999622,
0.370565343609427));
#12098=CARTESIAN_POINT('Ctrl Pts',(0.143314434899701,-0.0854943902146281,
0.366859690173333));
#12099=CARTESIAN_POINT('Ctrl Pts',(0.115057433514238,-0.132870992729294,
0.363154036737239));
#12100=CARTESIAN_POINT('Ctrl Pts',(0.0609790756413814,-0.164836359689817,
0.359448383301144));
#12101=CARTESIAN_POINT('Ctrl Pts',(0.0058505342293925,-0.16676871854526,
0.35574272986505));
#12102=CARTESIAN_POINT('Ctrl Pts',(-0.0492780071825968,-0.168701077400703,
0.352037076428955));
#12103=CARTESIAN_POINT('Ctrl Pts',(-0.105456732133718,-0.140600428151066,
0.348331422992861));
#12104=CARTESIAN_POINT('Ctrl Pts',(-0.136966392307533,-0.0953260539355553,
0.344625769556767));
#12105=CARTESIAN_POINT('Ctrl Pts',(-0.156165914113924,-0.0677393922506487,
0.342367834258171));
#12106=CARTESIAN_POINT('Ctrl Pts',(-0.166206477852866,-0.0337765899116774,
0.340109898959575));
#12107=CARTESIAN_POINT('Ctrl Pts',(-0.166378928688253,9.26016813348553E-5,
0.337851963660979));
#12108=CARTESIAN_POINT('Origin',(0.,0.,0.554592528053768));
#12109=CARTESIAN_POINT('',(-0.205542557565044,0.000180865543328967,0.0354074719462324));
#12110=CARTESIAN_POINT('',(-0.205288744110104,-0.000151770750953058,0.0295925280537678));
#12111=CARTESIAN_POINT('',(-0.205475,1.04123167373875E-16,0.554592528053768));
#12112=CARTESIAN_POINT('',(0.181742788875946,0.0958620587959239,0.));
#12113=CARTESIAN_POINT('Ctrl Pts',(-0.205288744110104,-0.000151770750953056,
0.0295925280537678));
#12114=CARTESIAN_POINT('Ctrl Pts',(-0.204996003270372,0.0451941134373501,
0.0271396589080337));
#12115=CARTESIAN_POINT('Ctrl Pts',(-0.16789984592073,0.159522204476035,
0.0209811363262054));
#12116=CARTESIAN_POINT('Ctrl Pts',(0.0215757967252497,0.241850803896632,
0.0111169603082828));
#12117=CARTESIAN_POINT('Ctrl Pts',(0.149857277933222,0.156313104352978,
0.00370565343609428));
#12118=CARTESIAN_POINT('Ctrl Pts',(0.181742788875947,0.0958620587959227,
0.));
#12119=CARTESIAN_POINT('',(0.205712120425506,-0.00753776543806376,-7.73744768374671E-17));
#12120=CARTESIAN_POINT('Origin',(0.,0.,0.));
#12121=CARTESIAN_POINT('Ctrl Pts',(-0.205542557565044,0.000180865543328964,
0.0354074719462324));
#12122=CARTESIAN_POINT('Ctrl Pts',(-0.205671097444409,0.014104284209969,
0.0346517512397107));
#12123=CARTESIAN_POINT('Ctrl Pts',(-0.198029895298052,0.0961615295363027,
0.0301903770970948));
#12124=CARTESIAN_POINT('Ctrl Pts',(-0.0876598130547602,0.226510042114602,
0.0220233495183845));
#12125=CARTESIAN_POINT('Ctrl Pts',(0.1412439463355,0.196648073709114,0.0109765795761622));
#12126=CARTESIAN_POINT('Ctrl Pts',(0.20807884879869,0.0591805639213882,
0.00363546307003382));
#12127=CARTESIAN_POINT('Ctrl Pts',(0.205712194497466,-0.00753777023904147,
-9.75646429965393E-17));
#12128=CARTESIAN_POINT('Origin',(0.,0.,0.554592528053768));
#12129=CARTESIAN_POINT('',(-0.205137705209698,-7.29564938461991E-7,0.105407471946233));
#12130=CARTESIAN_POINT('',(-0.205796175862248,-5.19920159535992E-5,0.0995925280537679));
#12131=CARTESIAN_POINT('',(-0.205475,1.04123167373875E-16,0.554592528053768));
#12132=CARTESIAN_POINT('Ctrl Pts',(-0.205796175862248,-5.19920159536016E-5,
0.0995925280537679));
#12133=CARTESIAN_POINT('Ctrl Pts',(-0.205575893814401,0.065178743908085,
0.0960402461912661));
#12134=CARTESIAN_POINT('Ctrl Pts',(-0.136801184004399,0.198857914726747,
0.0887823108926702));
#12135=CARTESIAN_POINT('Ctrl Pts',(0.0909120711847139,0.225228838155139,
0.0778187221579794));
#12136=CARTESIAN_POINT('Ctrl Pts',(0.238532429865686,0.0457136341101189,
0.0667017618496969));
#12137=CARTESIAN_POINT('Ctrl Pts',(0.167749407629896,-0.175679414345444,
0.0555848015414138));
#12138=CARTESIAN_POINT('Ctrl Pts',(-0.056737317834033,-0.236160773940692,
0.0444678412331312));
#12139=CARTESIAN_POINT('Ctrl Pts',(-0.19107773121668,-0.114782008526112,
0.0358037500705825));
#12140=CARTESIAN_POINT('Ctrl Pts',(-0.205438259271075,-0.0233118367668669,
0.030845312344128));
#12141=CARTESIAN_POINT('Ctrl Pts',(-0.205288744110104,-0.000151770750953056,
0.0295925280537678));
#12142=CARTESIAN_POINT('Ctrl Pts',(-0.205137705209698,-7.29564938455052E-7,
0.105407471946233));
#12143=CARTESIAN_POINT('Ctrl Pts',(-0.205136713680842,0.0343461846931921,
0.103552338522943));
#12144=CARTESIAN_POINT('Ctrl Pts',(-0.180678665067047,0.137302931168816,
0.0979915516635594));
#12145=CARTESIAN_POINT('Ctrl Pts',(-0.0178086481209368,0.24223078753445,
0.0887251113680815));
#12146=CARTESIAN_POINT('Ctrl Pts',(0.193892484656356,0.146279454291081,
0.0776081510597986));
#12147=CARTESIAN_POINT('Ctrl Pts',(0.228035008840565,-0.083631262664263,
0.0664911907515159));
#12148=CARTESIAN_POINT('Ctrl Pts',(0.0533337265757384,-0.236956827852518,
0.0553742304432329));
#12149=CARTESIAN_POINT('Ctrl Pts',(-0.154992928561183,-0.177602262622348,
0.0450129908414718));
#12150=CARTESIAN_POINT('Ctrl Pts',(-0.205040806066213,-0.0541687745787603,
0.038357404675805));
#12151=CARTESIAN_POINT('Ctrl Pts',(-0.205542557565044,0.000180865543328964,
0.0354074719462324));
#12152=CARTESIAN_POINT('Origin',(0.,0.,0.554592528053768));
#12153=CARTESIAN_POINT('',(-0.205537743537834,-0.000182726579705819,0.175407471946233));
#12154=CARTESIAN_POINT('',(-0.205429022845128,0.000187467295045848,0.169592528053768));
#12155=CARTESIAN_POINT('',(-0.205475,1.04123167373875E-16,0.554592528053768));
#12156=CARTESIAN_POINT('Ctrl Pts',(-0.205429022845128,0.000187467295045865,
0.169592528053768));
#12157=CARTESIAN_POINT('Ctrl Pts',(-0.205585846213551,0.0176404542992278,
0.168646486910593));
#12158=CARTESIAN_POINT('Ctrl Pts',(-0.195561570894733,0.103279499333914,
0.163994792331323));
#12159=CARTESIAN_POINT('Ctrl Pts',(-0.0759861566816445,0.230692308120466,
0.155637444315959));
#12160=CARTESIAN_POINT('Ctrl Pts',(0.152660865452576,0.188911355652872,
0.144520484007676));
#12161=CARTESIAN_POINT('Ctrl Pts',(0.241502185356776,-0.0258725193599183,
0.133403523699394));
#12162=CARTESIAN_POINT('Ctrl Pts',(0.109179165064989,-0.216962892225182,
0.122286563391111));
#12163=CARTESIAN_POINT('Ctrl Pts',(-0.123130670689012,-0.209360343050761,
0.111169603082828));
#12164=CARTESIAN_POINT('Ctrl Pts',(-0.204476509229018,-0.0737226253751628,
0.103604924637047));
#12165=CARTESIAN_POINT('Ctrl Pts',(-0.205805686651544,-0.00286836216970447,
0.0997458996273603));
#12166=CARTESIAN_POINT('Ctrl Pts',(-0.205796175862248,-5.19920159536016E-5,
0.0995925280537679));
#12167=CARTESIAN_POINT('Ctrl Pts',(-0.205537743537834,-0.00018272657970583,
0.175407471946233));
#12168=CARTESIAN_POINT('Ctrl Pts',(-0.20503593067685,0.0542502838243898,
0.172452925806175));
#12169=CARTESIAN_POINT('Ctrl Pts',(-0.154875836490767,0.177771618514381,
0.165792726230024));
#12170=CARTESIAN_POINT('Ctrl Pts',(0.0536344200204105,0.236888489580304,
0.155426873217778));
#12171=CARTESIAN_POINT('Ctrl Pts',(0.228135366692393,0.0833488984919273,
0.144309912909495));
#12172=CARTESIAN_POINT('Ctrl Pts',(0.193712423773769,-0.146520715699965,
0.133192952601213));
#12173=CARTESIAN_POINT('Ctrl Pts',(-0.0181106010581924,-0.24220824221319,
0.12207599229293));
#12174=CARTESIAN_POINT('Ctrl Pts',(-0.18076764144762,-0.137130727182572,
0.112814165407936));
#12175=CARTESIAN_POINT('Ctrl Pts',(-0.205138694272785,-0.0342622287190314,
0.107257991959037));
#12176=CARTESIAN_POINT('Ctrl Pts',(-0.205137705209698,-7.29564938455052E-7,
0.105407471946233));
#12177=CARTESIAN_POINT('Origin',(0.,0.,0.554592528053768));
#12178=CARTESIAN_POINT('',(-0.205737948496796,0.000110742126799651,0.245407471946232));
#12179=CARTESIAN_POINT('',(-0.205152667291151,-5.77023530759702E-5,0.239592528053768));
#12180=CARTESIAN_POINT('',(-0.205475,1.04123167373875E-16,0.554592528053768));
#12181=CARTESIAN_POINT('Ctrl Pts',(-0.205152667291151,-5.77023530759641E-5,
0.239592528053768));
#12182=CARTESIAN_POINT('Ctrl Pts',(-0.205057481701977,0.0378060063320381,
0.237547074193825));
#12183=CARTESIAN_POINT('Ctrl Pts',(-0.17685871883546,0.144397474870061,
0.231795966897788));
#12184=CARTESIAN_POINT('Ctrl Pts',(-0.00537745351023951,0.242824828130405,
0.222339206165656));
#12185=CARTESIAN_POINT('Ctrl Pts',(0.201133153391932,0.136155326051799,
0.211222245857373));
#12186=CARTESIAN_POINT('Ctrl Pts',(0.223448082612567,-0.0952038262864637,
0.20010528554909));
#12187=CARTESIAN_POINT('Ctrl Pts',(0.0411315804786337,-0.23937629702844,
0.188988325240808));
#12188=CARTESIAN_POINT('Ctrl Pts',(-0.160132400758511,-0.170716737438922,
0.1788174060757));
#12189=CARTESIAN_POINT('Ctrl Pts',(-0.204971567375627,-0.0507230854143627,
0.172352140346687));
#12190=CARTESIAN_POINT('Ctrl Pts',(-0.205429022845128,0.000187467295045865,
0.169592528053768));
#12191=CARTESIAN_POINT('Ctrl Pts',(-0.205737948496796,0.00011074212679966,
0.245407471946232));
#12192=CARTESIAN_POINT('Ctrl Pts',(-0.205779614688409,0.00651151311194001,
0.245059166525502));
#12193=CARTESIAN_POINT('Ctrl Pts',(-0.202604460038461,0.0809687895657837,
0.241005207668677));
#12194=CARTESIAN_POINT('Ctrl Pts',(-0.111975498770539,0.215532531397883,
0.233245595375758));
#12195=CARTESIAN_POINT('Ctrl Pts',(0.120411794779082,0.210935552206459,
0.222128635067475));
#12196=CARTESIAN_POINT('Ctrl Pts',(0.242527242701154,0.0131659096813392,
0.211011674759192));
#12197=CARTESIAN_POINT('Ctrl Pts',(0.142538726865704,-0.196660905158453,
0.199894714450909));
#12198=CARTESIAN_POINT('Ctrl Pts',(-0.087985280286033,-0.226387709039377,
0.188777754142627));
#12199=CARTESIAN_POINT('Ctrl Pts',(-0.198081706594962,-0.0959907227805277,
0.180615339974401));
#12200=CARTESIAN_POINT('Ctrl Pts',(-0.205665314840926,-0.0140207339492534,
0.17615857924227));
#12201=CARTESIAN_POINT('Ctrl Pts',(-0.205537743537834,-0.00018272657970583,
0.175407471946233));
#12202=CARTESIAN_POINT('Origin',(0.,0.,0.554592528053768));
#12203=CARTESIAN_POINT('',(-0.205202343170581,0.000114209666698867,0.315407471946233));
#12204=CARTESIAN_POINT('',(-0.205640730232501,-0.000158877854750073,0.309592528053768));
#12205=CARTESIAN_POINT('',(-0.205475,1.04123167373875E-16,0.554592528053768));
#12206=CARTESIAN_POINT('Ctrl Pts',(-0.205640730232501,-0.000158877854750081,
0.309592528053768));
#12207=CARTESIAN_POINT('Ctrl Pts',(-0.205147522672671,0.0577055172922507,
0.306447661477057));
#12208=CARTESIAN_POINT('Ctrl Pts',(-0.149444666487041,0.184584641155565,
0.299597141464252));
#12209=CARTESIAN_POINT('Ctrl Pts',(0.0656990433896697,0.233829699755635,
0.289040968015353));
#12210=CARTESIAN_POINT('Ctrl Pts',(0.232105615114709,0.0715529424102004,
0.27792400770707));
#12211=CARTESIAN_POINT('Ctrl Pts',(0.185952226875698,-0.156251740320434,
0.266807047398788));
#12212=CARTESIAN_POINT('Ctrl Pts',(-0.030494276369136,-0.240962440043193,
0.255690087090504));
#12213=CARTESIAN_POINT('Ctrl Pts',(-0.18432786741861,-0.130018191841,0.246618580642165));
#12214=CARTESIAN_POINT('Ctrl Pts',(-0.205229924998058,-0.0307899101733451,
0.241252727629919));
#12215=CARTESIAN_POINT('Ctrl Pts',(-0.205152667291151,-5.77023530759641E-5,
0.239592528053768));
#12216=CARTESIAN_POINT('Ctrl Pts',(-0.205202343170581,0.000114209666698874,
0.315407471946233));
#12217=CARTESIAN_POINT('Ctrl Pts',(-0.205338714105211,0.0268973406518496,
0.313959753808734));
#12218=CARTESIAN_POINT('Ctrl Pts',(-0.188013873562118,0.122066992862534,
0.308806382235141));
#12219=CARTESIAN_POINT('Ctrl Pts',(-0.0442230349178335,0.238822732453524,
0.299947357225455));
#12220=CARTESIAN_POINT('Ctrl Pts',(0.176712068309585,0.166630571298318,
0.288830396917172));
#12221=CARTESIAN_POINT('Ctrl Pts',(0.235817802334529,-0.0581630255277868,
0.277713436608889));
#12222=CARTESIAN_POINT('Ctrl Pts',(0.078963123396891,-0.229690015875461,
0.266596476300606));
#12223=CARTESIAN_POINT('Ctrl Pts',(-0.143024641581339,-0.192086316597046,
0.255827821413055));
#12224=CARTESIAN_POINT('Ctrl Pts',(-0.205336324240059,-0.0615868786529226,
0.248764819961596));
#12225=CARTESIAN_POINT('Ctrl Pts',(-0.205737948496796,0.00011074212679966,
0.245407471946232));
#12226=CARTESIAN_POINT('Origin',(0.,0.,0.554592528053768));
#12227=CARTESIAN_POINT('',(-0.205269929560708,-0.000254221530507082,0.385407471946233));
#12228=CARTESIAN_POINT('',(-0.205652323534904,0.00014910722334396,0.379592528053768));
#12229=CARTESIAN_POINT('',(-0.205475,1.04123167373875E-16,0.554592528053768));
#12230=CARTESIAN_POINT('',(-0.053017021718863,-0.198517432567172,0.4));
#12231=CARTESIAN_POINT('Ctrl Pts',(-0.0530170217188623,-0.198517432567172,
0.4));
#12232=CARTESIAN_POINT('Ctrl Pts',(-0.11904762702766,-0.180882981070921,
0.396294346563906));
#12233=CARTESIAN_POINT('Ctrl Pts',(-0.192514897068364,-0.111293028538514,
0.391430170545983));
#12234=CARTESIAN_POINT('Ctrl Pts',(-0.205432812329624,-0.0216624454594562,
0.386565994528061));
#12235=CARTESIAN_POINT('Ctrl Pts',(-0.205269929560708,-0.000254221530507089,
0.385407471946233));
#12236=CARTESIAN_POINT('',(0.0531240965569158,-0.198877135945741,0.4));
#12237=CARTESIAN_POINT('Origin',(0.,0.,0.4));
#12238=CARTESIAN_POINT('Ctrl Pts',(0.0531241180331692,-0.198877208092298,
0.4));
#12239=CARTESIAN_POINT('Ctrl Pts',(-0.0113947906349914,-0.216030727448873,
0.396364536929966));
#12240=CARTESIAN_POINT('Ctrl Pts',(-0.149363620668702,-0.183997545270092,
0.389562046281222));
#12241=CARTESIAN_POINT('Ctrl Pts',(-0.205163206243598,-0.0580990125538643,
0.382759555632478));
#12242=CARTESIAN_POINT('Ctrl Pts',(-0.205652323534904,0.000149107223343921,
0.379592528053768));
#12243=CARTESIAN_POINT('Origin',(0.,0.,0.554592528053768));
#12244=CARTESIAN_POINT('Ctrl Pts',(-0.205652323534904,0.000149107223343921,
0.379592528053768));
#12245=CARTESIAN_POINT('Ctrl Pts',(-0.20573550917628,0.010055539256624,
0.379053902196384));
#12246=CARTESIAN_POINT('Ctrl Pts',(-0.200581379579465,0.0880330322633288,
0.374809622902905));
#12247=CARTESIAN_POINT('Ctrl Pts',(-0.100785874709386,0.221009791285371,
0.366859690173332));
#12248=CARTESIAN_POINT('Ctrl Pts',(0.131058487025979,0.204477699076557,
0.35574272986505));
#12249=CARTESIAN_POINT('Ctrl Pts',(0.242883715861565,0.000731295485493303,
0.344625769556767));
#12250=CARTESIAN_POINT('Ctrl Pts',(0.13227703569284,-0.20370800021477,0.333508809248484));
#12251=CARTESIAN_POINT('Ctrl Pts',(-0.0994668003959092,-0.221581469162487,
0.322391848940201));
#12252=CARTESIAN_POINT('Ctrl Pts',(-0.200331019397092,-0.0888856881277869,
0.314419755208629));
#12253=CARTESIAN_POINT('Ctrl Pts',(-0.205728678103024,-0.0104771510256757,
0.310153314913151));
#12254=CARTESIAN_POINT('Ctrl Pts',(-0.205640730232501,-0.000158877854750081,
0.309592528053768));
#12255=CARTESIAN_POINT('Ctrl Pts',(-0.205269929560708,-0.000254221530507089,
0.385407471946233));
#12256=CARTESIAN_POINT('Ctrl Pts',(-0.204911815068299,0.046813956992531,
0.382860341091967));
#12257=CARTESIAN_POINT('Ctrl Pts',(-0.165590599079174,0.163076528415273,
0.376607556801606));
#12258=CARTESIAN_POINT('Ctrl Pts',(0.0274206054315193,0.241260887402562,
0.366649119075152));
#12259=CARTESIAN_POINT('Ctrl Pts',(0.217614460633585,0.107865604001965,
0.355532158766869));
#12260=CARTESIAN_POINT('Ctrl Pts',(0.208602501412145,-0.124451281241526,
0.344415198458586));
#12261=CARTESIAN_POINT('Ctrl Pts',(0.00851095428263868,-0.242724098340208,
0.333298238150303));
#12262=CARTESIAN_POINT('Ctrl Pts',(-0.172282834993387,-0.152290880723065,
0.323628995979519));
#12263=CARTESIAN_POINT('Ctrl Pts',(-0.204989652081738,-0.0416581321254629,
0.317665407244829));
#12264=CARTESIAN_POINT('Ctrl Pts',(-0.205202343170581,0.000114209666698874,
0.315407471946233));
#12265=CARTESIAN_POINT('Ctrl Pts',(0.126907087985239,0.10793586530485,0.4));
#12266=CARTESIAN_POINT('Ctrl Pts',(0.162808572446542,0.0657241978997387,
0.396294346563906));
#12267=CARTESIAN_POINT('Ctrl Pts',(0.188558283864404,-0.0566085385263014,
0.388883039691717));
#12268=CARTESIAN_POINT('Ctrl Pts',(0.0543899581658451,-0.189407309917837,
0.377766079383434));
#12269=CARTESIAN_POINT('Ctrl Pts',(-0.129549863896177,-0.148244923123477,
0.366649119075152));
#12270=CARTESIAN_POINT('Ctrl Pts',(-0.194866319237398,0.0284258764902441,
0.355532158766869));
#12271=CARTESIAN_POINT('Ctrl Pts',(-0.0817176139510098,0.17919567454991,
0.344415198458586));
#12272=CARTESIAN_POINT('Ctrl Pts',(0.106262776194322,0.165791384188609,
0.333298238150303));
#12273=CARTESIAN_POINT('Ctrl Pts',(0.196931145212491,0.000592937476010039,
0.32218127784202));
#12274=CARTESIAN_POINT('Ctrl Pts',(0.107250780612859,-0.165167309092496,
0.311064317533737));
#12275=CARTESIAN_POINT('Ctrl Pts',(-0.0806481029125611,-0.179659193393213,
0.299947357225455));
#12276=CARTESIAN_POINT('Ctrl Pts',(-0.194690620681517,-0.0296261973875841,
0.288830396917171));
#12277=CARTESIAN_POINT('Ctrl Pts',(-0.130437300262912,0.147540865453661,
0.27771343660889));
#12278=CARTESIAN_POINT('Ctrl Pts',(0.0532690625561212,0.189590110618269,
0.266596476300606));
#12279=CARTESIAN_POINT('Ctrl Pts',(0.188192215491474,0.0580154286679129,
0.255479515992324));
#12280=CARTESIAN_POINT('Ctrl Pts',(0.150770852889604,-0.126689572636011,
0.24436255568404));
#12281=CARTESIAN_POINT('Ctrl Pts',(-0.0247248883956591,-0.195373366644097,
0.233245595375758));
#12282=CARTESIAN_POINT('Ctrl Pts',(-0.17757783936906,-0.0851363526373409,
0.222128635067475));
#12283=CARTESIAN_POINT('Ctrl Pts',(-0.167806831657998,0.103067710537421,
0.211011674759192));
#12284=CARTESIAN_POINT('Ctrl Pts',(-0.00436006207473383,0.196883398790731,
0.19989471445091));
#12285=CARTESIAN_POINT('Ctrl Pts',(0.163079612386402,0.110395314856939,
0.188777754142626));
#12286=CARTESIAN_POINT('Ctrl Pts',(0.18117265148195,-0.0771916654547992,
0.177660793834344));
#12287=CARTESIAN_POINT('Ctrl Pts',(0.0333496596069613,-0.194087315171861,
0.166543833526061));
#12288=CARTESIAN_POINT('Ctrl Pts',(-0.145014634580667,-0.133239796355326,
0.155426873217778));
#12289=CARTESIAN_POINT('Ctrl Pts',(-0.190575968723863,0.0496273376778148,
0.144309912909495));
#12290=CARTESIAN_POINT('Ctrl Pts',(-0.0616098975698358,0.18704630019647,
0.133192952601213));
#12291=CARTESIAN_POINT('Ctrl Pts',(0.123778076089058,0.153170127031359,
0.12207599229293));
#12292=CARTESIAN_POINT('Ctrl Pts',(0.195810994429682,-0.0209775482436421,
0.110959031984647));
#12293=CARTESIAN_POINT('Ctrl Pts',(0.0885229293092943,-0.175914431656968,
0.0998420716763641));
#12294=CARTESIAN_POINT('Ctrl Pts',(-0.099834869141207,-0.169750252596456,
0.0887251113680815));
#12295=CARTESIAN_POINT('Ctrl Pts',(-0.196762351281628,-0.00813138316770982,
0.0776081510597984));
#12296=CARTESIAN_POINT('Ctrl Pts',(-0.113501812995563,0.160935727486608,
0.0664911907515158));
#12297=CARTESIAN_POINT('Ctrl Pts',(0.0737118922466157,0.18261649561575,
0.0553742304432329));
#12298=CARTESIAN_POINT('Ctrl Pts',(0.193403104103289,0.0370648080922049,
0.0442572701349501));
#12299=CARTESIAN_POINT('Ctrl Pts',(0.136011929972701,-0.142441612994043,
0.0331403098266672));
#12300=CARTESIAN_POINT('Ctrl Pts',(-0.0460028575308428,-0.191480155437495,
0.0220233495183845));
#12301=CARTESIAN_POINT('Ctrl Pts',(-0.185763770878031,-0.0652038794595693,
0.0109063892101018));
#12302=CARTESIAN_POINT('Ctrl Pts',(-0.155645146477646,0.120863497291556,
-0.000210571098181166));
#12303=CARTESIAN_POINT('Ctrl Pts',(0.0174937473387352,0.19609365581788,
-0.0113275314064639));
#12304=CARTESIAN_POINT('Ctrl Pts',(0.121504915457719,0.126739326853418,
-0.0187388382786524));
#12305=CARTESIAN_POINT('Ctrl Pts',(0.147357822736259,0.0777253631604853,
-0.0224444917147467));
#12306=CARTESIAN_POINT('Ctrl Pts',(0.136778062465884,0.116331236980973,
0.407481497238249));
#12307=CARTESIAN_POINT('Ctrl Pts',(0.175472004327013,0.0708362991269342,
0.403775843802155));
#12308=CARTESIAN_POINT('Ctrl Pts',(0.203224556944093,-0.0610116136267615,
0.396364536929966));
#12309=CARTESIAN_POINT('Ctrl Pts',(0.0586204696178205,-0.204139621188457,
0.385247576621684));
#12310=CARTESIAN_POINT('Ctrl Pts',(-0.139626396427117,-0.159775578158341,
0.3741306163134));
#12311=CARTESIAN_POINT('Ctrl Pts',(-0.210023238325741,0.0306368727858788,
0.363013656005118));
#12312=CARTESIAN_POINT('Ctrl Pts',(-0.0880737008704687,0.19313371346173,
0.351896695696835));
#12313=CARTESIAN_POINT('Ctrl Pts',(0.114528013138208,0.178686822484592,
0.340779735388552));
#12314=CARTESIAN_POINT('Ctrl Pts',(0.212248668762182,0.000639056812504505,
0.32966277508027));
#12315=CARTESIAN_POINT('Ctrl Pts',(0.115592865639519,-0.178014206133254,
0.318545814771986));
#12316=CARTESIAN_POINT('Ctrl Pts',(-0.086921002073677,-0.193633285316304,
0.307428854463704));
#12317=CARTESIAN_POINT('Ctrl Pts',(-0.209833873740729,-0.031930555977905,
0.296311894155421));
#12318=CARTESIAN_POINT('Ctrl Pts',(-0.14058285858168,0.159016758099742,
0.285194933847138));
#12319=CARTESIAN_POINT('Ctrl Pts',(0.0574123895006371,0.204336640330724,
0.274077973538855));
#12320=CARTESIAN_POINT('Ctrl Pts',(0.202830015365886,0.0625279332486754,
0.262961013230573));
#12321=CARTESIAN_POINT('Ctrl Pts',(0.162497977551635,-0.136543628530819,
0.251844052922289));
#12322=CARTESIAN_POINT('Ctrl Pts',(-0.0266480177201514,-0.210569724443796,
0.240727092614007));
#12323=CARTESIAN_POINT('Ctrl Pts',(-0.19139004126076,-0.0917583528549811,
0.229610132305724));
#12324=CARTESIAN_POINT('Ctrl Pts',(-0.180859033700225,0.111084431720179,
0.218493171997441));
#12325=CARTESIAN_POINT('Ctrl Pts',(-0.00469919255323577,0.212197208570623,
0.207376211689158));
#12326=CARTESIAN_POINT('Ctrl Pts',(0.175764126054912,0.118981985255226,
0.196259251380876));
#12327=CARTESIAN_POINT('Ctrl Pts',(0.195264461858822,-0.083195719065354,
0.185142291072593));
#12328=CARTESIAN_POINT('Ctrl Pts',(0.0359436332308521,-0.209183642457387,
0.17402533076431));
#12329=CARTESIAN_POINT('Ctrl Pts',(-0.156294034179153,-0.143603335937786,
0.162908370456027));
#12330=CARTESIAN_POINT('Ctrl Pts',(-0.205399179576485,0.0534874072100777,
0.151791410147744));
#12331=CARTESIAN_POINT('Ctrl Pts',(-0.0664019839404387,0.201594969504469,
0.140674449839462));
#12332=CARTESIAN_POINT('Ctrl Pts',(0.133405672543564,0.165083869905196,
0.129557489531179));
#12333=CARTESIAN_POINT('Ctrl Pts',(0.21104139140538,-0.0226092052824009,
0.118440529222896));
#12334=CARTESIAN_POINT('Ctrl Pts',(0.0954083412278594,-0.189597251846372,
0.107323568914613));
#12335=CARTESIAN_POINT('Ctrl Pts',(-0.107600136323809,-0.182953616081225,
0.0962066086063303));
#12336=CARTESIAN_POINT('Ctrl Pts',(-0.212066745851603,-0.00876385119621063,
0.0850896482980474));
#12337=CARTESIAN_POINT('Ctrl Pts',(-0.12233011027488,0.173453487402658,
0.0739726879897647));
#12338=CARTESIAN_POINT('Ctrl Pts',(0.0794452852259816,0.196820609795546,
0.0628557276814818));
#12339=CARTESIAN_POINT('Ctrl Pts',(0.208446212690755,0.0399477500981762,
0.051738767373199));
#12340=CARTESIAN_POINT('Ctrl Pts',(0.146591089191766,-0.153520880111177,
0.0406218070649162));
#12341=CARTESIAN_POINT('Ctrl Pts',(-0.0495810109652396,-0.20637369493856,
0.0295048467566334));
#12342=CARTESIAN_POINT('Ctrl Pts',(-0.200212683628898,-0.0702755097396628,
0.0183878864483507));
#12343=CARTESIAN_POINT('Ctrl Pts',(-0.167751399117339,0.130264394564884,
0.00727092614006771));
#12344=CARTESIAN_POINT('Ctrl Pts',(0.0188544304675734,0.211346038510798,
-0.00384603416821501));
#12345=CARTESIAN_POINT('Ctrl Pts',(0.130955702949553,0.136597252686605,
-0.0112573410404035));
#12346=CARTESIAN_POINT('Ctrl Pts',(0.158819478116155,0.0837709283722978,
-0.0149629944764978));
#12347=CARTESIAN_POINT('Ctrl Pts',(0.146649036946528,0.124726608657095,
0.414962994476498));
#12348=CARTESIAN_POINT('Ctrl Pts',(0.188135436207484,0.0759484003541298,
0.411257341040404));
#12349=CARTESIAN_POINT('Ctrl Pts',(0.217890830023782,-0.0654146887272218,
0.403846034168215));
#12350=CARTESIAN_POINT('Ctrl Pts',(0.0628509810697956,-0.218871932459077,
0.392729073859932));
#12351=CARTESIAN_POINT('Ctrl Pts',(-0.149702928958057,-0.171306233193206,
0.38161211355165));
#12352=CARTESIAN_POINT('Ctrl Pts',(-0.225180157414084,0.0328478690815136,
0.370495153243366));
#12353=CARTESIAN_POINT('Ctrl Pts',(-0.0944297877899273,0.207071752373551,
0.359378192935084));
#12354=CARTESIAN_POINT('Ctrl Pts',(0.122793250082094,0.191582260780575,
0.348261232626801));
#12355=CARTESIAN_POINT('Ctrl Pts',(0.227566192311873,0.000685176148998803,
0.337144272318518));
#12356=CARTESIAN_POINT('Ctrl Pts',(0.12393495066618,-0.190861103174011,
0.326027312010235));
#12357=CARTESIAN_POINT('Ctrl Pts',(-0.0931939012347931,-0.207607377239396,
0.314910351701953));
#12358=CARTESIAN_POINT('Ctrl Pts',(-0.224977126799941,-0.0342349145682256,
0.303793391393669));
#12359=CARTESIAN_POINT('Ctrl Pts',(-0.150728416900449,0.170492650745823,
0.292676431085387));
#12360=CARTESIAN_POINT('Ctrl Pts',(0.0615557164451535,0.21908317004318,
0.281559470777104));
#12361=CARTESIAN_POINT('Ctrl Pts',(0.217467815240298,0.067040437829438,
0.270442510468822));
#12362=CARTESIAN_POINT('Ctrl Pts',(0.174225102213667,-0.146397684425626,
0.259325550160538));
#12363=CARTESIAN_POINT('Ctrl Pts',(-0.0285711470446437,-0.225766082243494,
0.248208589852256));
#12364=CARTESIAN_POINT('Ctrl Pts',(-0.205202243152462,-0.0983803530726217,
0.237091629543973));
#12365=CARTESIAN_POINT('Ctrl Pts',(-0.193911235742451,0.119101152902937,
0.22597466923569));
#12366=CARTESIAN_POINT('Ctrl Pts',(-0.00503832303173776,0.227511018350514,
0.214857708927407));
#12367=CARTESIAN_POINT('Ctrl Pts',(0.188448639723422,0.127568655653512,
0.203740748619124));
#12368=CARTESIAN_POINT('Ctrl Pts',(0.209356272235695,-0.0891997726759089,
0.192623788310842));
#12369=CARTESIAN_POINT('Ctrl Pts',(0.038537606854743,-0.224279969742913,
0.181506828002559));
#12370=CARTESIAN_POINT('Ctrl Pts',(-0.16757343377764,-0.153966875520245,
0.170389867694276));
#12371=CARTESIAN_POINT('Ctrl Pts',(-0.220222390429106,0.0573474767423407,
0.159272907385993));
#12372=CARTESIAN_POINT('Ctrl Pts',(-0.0711940703110417,0.216143638812467,
0.14815594707771));
#12373=CARTESIAN_POINT('Ctrl Pts',(0.14303326899807,0.176997612779034,0.137038986769428));
#12374=CARTESIAN_POINT('Ctrl Pts',(0.226271788381078,-0.0242408623211596,
0.125922026461145));
#12375=CARTESIAN_POINT('Ctrl Pts',(0.102293753146424,-0.203280072035777,
0.114805066152862));
#12376=CARTESIAN_POINT('Ctrl Pts',(-0.115365403506411,-0.196156979565993,
0.103688105844579));
#12377=CARTESIAN_POINT('Ctrl Pts',(-0.227371140421577,-0.00939631922471147,
0.0925711455362963));
#12378=CARTESIAN_POINT('Ctrl Pts',(-0.131158407554197,0.185971247318709,
0.0814541852280135));
#12379=CARTESIAN_POINT('Ctrl Pts',(0.0851786782053478,0.211024723975343,
0.0703372249197307));
#12380=CARTESIAN_POINT('Ctrl Pts',(0.22348932127822,0.0428306921041475,
0.0592202646114479));
#12381=CARTESIAN_POINT('Ctrl Pts',(0.157170248410831,-0.16460014722831,
0.048103304303165));
#12382=CARTESIAN_POINT('Ctrl Pts',(-0.0531591643996364,-0.221267234439626,
0.0369863439948823));
#12383=CARTESIAN_POINT('Ctrl Pts',(-0.214661596379765,-0.0753471400197565,
0.0258693836865995));
#12384=CARTESIAN_POINT('Ctrl Pts',(-0.179857651757032,0.139665291838212,
0.0147524233783167));
#12385=CARTESIAN_POINT('Ctrl Pts',(0.0202151135964117,0.226598421203715,
0.00363546307003391));
#12386=CARTESIAN_POINT('Ctrl Pts',(0.140406490441387,0.146455178519791,
-0.00377584380215461));
#12387=CARTESIAN_POINT('Ctrl Pts',(0.170281133496051,0.0898164935841102,
-0.00748149723824889));
#12388=CARTESIAN_POINT('Ctrl Pts',(0.156520011427173,0.133121980333218,
0.422444491714747));
#12389=CARTESIAN_POINT('Ctrl Pts',(0.200798868087955,0.0810605015813253,
0.418738838278652));
#12390=CARTESIAN_POINT('Ctrl Pts',(0.232557103103471,-0.0698177638276817,
0.411327531406463));
#12391=CARTESIAN_POINT('Ctrl Pts',(0.0670814925217709,-0.233604243729697,
0.400210571098181));
#12392=CARTESIAN_POINT('Ctrl Pts',(-0.159779461488997,-0.18283688822807,
0.389093610789898));
#12393=CARTESIAN_POINT('Ctrl Pts',(-0.240337076502428,0.0350588653771482,
0.377976650481616));
#12394=CARTESIAN_POINT('Ctrl Pts',(-0.100785874709386,0.221009791285371,
0.366859690173332));
#12395=CARTESIAN_POINT('Ctrl Pts',(0.131058487025979,0.204477699076557,
0.35574272986505));
#12396=CARTESIAN_POINT('Ctrl Pts',(0.242883715861565,0.000731295485493303,
0.344625769556767));
#12397=CARTESIAN_POINT('Ctrl Pts',(0.13227703569284,-0.20370800021477,0.333508809248484));
#12398=CARTESIAN_POINT('Ctrl Pts',(-0.0994668003959092,-0.221581469162487,
0.322391848940201));
#12399=CARTESIAN_POINT('Ctrl Pts',(-0.240120379859152,-0.0365392731585464,
0.311274888631918));
#12400=CARTESIAN_POINT('Ctrl Pts',(-0.160873975219218,0.181968543391903,
0.300157928323636));
#12401=CARTESIAN_POINT('Ctrl Pts',(0.0656990433896697,0.233829699755635,
0.289040968015353));
#12402=CARTESIAN_POINT('Ctrl Pts',(0.232105615114709,0.0715529424102004,
0.27792400770707));
#12403=CARTESIAN_POINT('Ctrl Pts',(0.185952226875698,-0.156251740320434,
0.266807047398788));
#12404=CARTESIAN_POINT('Ctrl Pts',(-0.030494276369136,-0.240962440043193,
0.255690087090504));
#12405=CARTESIAN_POINT('Ctrl Pts',(-0.219014445044163,-0.105002353290262,
0.244573126782222));
#12406=CARTESIAN_POINT('Ctrl Pts',(-0.206963437784677,0.127117874085694,
0.233456166473939));
#12407=CARTESIAN_POINT('Ctrl Pts',(-0.00537745351023951,0.242824828130405,
0.222339206165656));
#12408=CARTESIAN_POINT('Ctrl Pts',(0.201133153391932,0.136155326051799,
0.211222245857373));
#12409=CARTESIAN_POINT('Ctrl Pts',(0.223448082612567,-0.0952038262864637,
0.20010528554909));
#12410=CARTESIAN_POINT('Ctrl Pts',(0.0411315804786337,-0.23937629702844,
0.188988325240808));
#12411=CARTESIAN_POINT('Ctrl Pts',(-0.178852833376126,-0.164330415102705,
0.177871364932525));
#12412=CARTESIAN_POINT('Ctrl Pts',(-0.235045601281728,0.0612075462746037,
0.166754404624242));
#12413=CARTESIAN_POINT('Ctrl Pts',(-0.0759861566816445,0.230692308120466,
0.155637444315959));
#12414=CARTESIAN_POINT('Ctrl Pts',(0.152660865452576,0.188911355652872,
0.144520484007676));
#12415=CARTESIAN_POINT('Ctrl Pts',(0.241502185356776,-0.0258725193599183,
0.133403523699394));
#12416=CARTESIAN_POINT('Ctrl Pts',(0.109179165064989,-0.216962892225182,
0.122286563391111));
#12417=CARTESIAN_POINT('Ctrl Pts',(-0.123130670689012,-0.209360343050761,
0.111169603082828));
#12418=CARTESIAN_POINT('Ctrl Pts',(-0.242675534991552,-0.0100287872532125,
0.100052642774545));
#12419=CARTESIAN_POINT('Ctrl Pts',(-0.139986704833514,0.198489007234759,
0.0889356824662626));
#12420=CARTESIAN_POINT('Ctrl Pts',(0.0909120711847139,0.225228838155139,
0.0778187221579794));
#12421=CARTESIAN_POINT('Ctrl Pts',(0.238532429865686,0.0457136341101189,
0.0667017618496969));
#12422=CARTESIAN_POINT('Ctrl Pts',(0.167749407629896,-0.175679414345444,
0.0555848015414138));
#12423=CARTESIAN_POINT('Ctrl Pts',(-0.056737317834033,-0.236160773940692,
0.0444678412331312));
#12424=CARTESIAN_POINT('Ctrl Pts',(-0.229110509130633,-0.0804187702998499,
0.0333508809248484));
#12425=CARTESIAN_POINT('Ctrl Pts',(-0.191963904396724,0.14906618911154,
0.0222339206165656));
#12426=CARTESIAN_POINT('Ctrl Pts',(0.0215757967252497,0.241850803896632,
0.0111169603082828));
#12427=CARTESIAN_POINT('Ctrl Pts',(0.149857277933222,0.156313104352978,
0.00370565343609428));
#12428=CARTESIAN_POINT('Ctrl Pts',(0.181742788875947,0.0958620587959227,
0.));
#12429=CARTESIAN_POINT('Ctrl Pts',(0.181742788875947,0.0958620587959227,
0.));
#12430=CARTESIAN_POINT('Ctrl Pts',(0.174504469275116,0.106933967990933,
1.09227492917999E-17));
#12431=CARTESIAN_POINT('Ctrl Pts',(0.166155260988786,0.117183932421154,
8.28421226973214E-17));
#12432=CARTESIAN_POINT('Ctrl Pts',(0.156880171408913,0.126533297038658,
1.45716771982052E-16));
#12433=CARTESIAN_POINT('Ctrl Pts',(0.152161070776583,0.131290188290046,
1.77706953278083E-16));
#12434=CARTESIAN_POINT('Ctrl Pts',(0.147201652193067,0.135813345993139,
6.21654697047341E-17));
#12435=CARTESIAN_POINT('Ctrl Pts',(0.142023529523608,0.140088211751239,
9.71445146547012E-17));
#12436=CARTESIAN_POINT('Ctrl Pts',(0.138407013399961,0.143073873143886,
1.21574658188656E-16));
#12437=CARTESIAN_POINT('Ctrl Pts',(0.134683780798487,0.145938358461697,
2.40181658122892E-17));
#12438=CARTESIAN_POINT('Ctrl Pts',(0.130860959346397,0.148675760328277,
3.46944695195361E-18));
#12439=CARTESIAN_POINT('Ctrl Pts',(0.127608826692069,0.151004509946822,
-1.40116623407028E-17));
#12440=CARTESIAN_POINT('Ctrl Pts',(0.124283670899528,0.153241554310962,
1.50905609184793E-16));
#12441=CARTESIAN_POINT('Ctrl Pts',(0.120904294225889,0.155374611387964,
1.45716771982052E-16));
#12442=CARTESIAN_POINT('Ctrl Pts',(0.109987742648693,0.162265121043141,
1.2895503914793E-16));
#12443=CARTESIAN_POINT('Ctrl Pts',(0.0984734851501926,0.168099067174435,
6.42435548254899E-17));
#12444=CARTESIAN_POINT('Ctrl Pts',(0.0865220202785484,0.172774083264826,
1.21430643318376E-16));
#12445=CARTESIAN_POINT('Ctrl Pts',(0.0785613376854963,0.175888037881495,
1.5952206263826E-16));
#12446=CARTESIAN_POINT('Ctrl Pts',(0.0704062138058044,0.178486876003788,
2.3171885042452E-16));
#12447=CARTESIAN_POINT('Ctrl Pts',(0.0621035437179694,0.180527190751547,
3.17454396103756E-16));
#12448=CARTESIAN_POINT('Ctrl Pts',(0.058507058441047,0.181410998234318,
3.5459264494205E-16));
#12449=CARTESIAN_POINT('Ctrl Pts',(0.0548830801400362,0.182189535865417,
2.01904242815308E-16));
#12450=CARTESIAN_POINT('Ctrl Pts',(0.0512492809662162,0.18285695898382,
2.04697370165263E-16));
#12451=CARTESIAN_POINT('Ctrl Pts',(0.0397135857002833,0.184975730368547,
2.13564306505654E-16));
#12452=CARTESIAN_POINT('Ctrl Pts',(0.028043543428156,0.185987354367647,
2.12494214757903E-16));
#12453=CARTESIAN_POINT('Ctrl Pts',(0.0163641619208267,0.185791435560747,
1.37043154602168E-16));
#12454=CARTESIAN_POINT('Ctrl Pts',(0.0073677207352634,0.185640522430431,
7.89876483687746E-17));
#12455=CARTESIAN_POINT('Ctrl Pts',(-0.00163453813548323,0.184771897471103,
1.62267606068596E-16));
#12456=CARTESIAN_POINT('Ctrl Pts',(-0.0105685044145391,0.183215538396018,
1.40512601554121E-16));
#12457=CARTESIAN_POINT('Ctrl Pts',(-0.0140598689340656,0.182607318408986,
1.32010817630666E-16));
#12458=CARTESIAN_POINT('Ctrl Pts',(-0.0175381431895957,0.181894183787698,
7.91699990801813E-17));
#12459=CARTESIAN_POINT('Ctrl Pts',(-0.0209886167262666,0.181080905311167,
7.63278329429795E-17));
#12460=CARTESIAN_POINT('Ctrl Pts',(-0.0323062471842877,0.178413333698454,
6.70054643755085E-17));
#12461=CARTESIAN_POINT('Ctrl Pts',(-0.0433589456433749,0.17466582100756,
6.12246176381618E-17));
#12462=CARTESIAN_POINT('Ctrl Pts',(-0.0539912114056113,0.169918461793345,
1.11889664200504E-16));
#12463=CARTESIAN_POINT('Ctrl Pts',(-0.0600125950487974,0.16722988423518,
1.40582859938265E-16));
#12464=CARTESIAN_POINT('Ctrl Pts',(-0.0658987875201912,0.164219919342787,
2.24249992830267E-17));
#12465=CARTESIAN_POINT('Ctrl Pts',(-0.0716172696707604,0.160898707475948,
4.33680868994202E-18));
#12466=CARTESIAN_POINT('Ctrl Pts',(-0.0760153027671363,0.158344393354502,
-9.57465571395114E-18));
#12467=CARTESIAN_POINT('Ctrl Pts',(-0.0803162508173771,0.155603868531732,
-1.48983259173674E-17));
#12468=CARTESIAN_POINT('Ctrl Pts',(-0.0844844353506574,0.152695748064502,
3.38271077815477E-17));
#12469=CARTESIAN_POINT('Ctrl Pts',(-0.0920276705150646,0.147432872489875,
1.22006362309274E-16));
#12470=CARTESIAN_POINT('Ctrl Pts',(-0.099152018847274,0.141614034257408,
8.85855526066679E-17));
#12471=CARTESIAN_POINT('Ctrl Pts',(-0.105766305686817,0.135269691928801,
6.85215773010839E-17));
#12472=CARTESIAN_POINT('Ctrl Pts',(-0.109162917311535,0.132011703966182,
5.82181941224795E-17));
#12473=CARTESIAN_POINT('Ctrl Pts',(-0.112424939305554,0.1286141740075,1.36999553352078E-16));
#12474=CARTESIAN_POINT('Ctrl Pts',(-0.115528518436688,0.125092942690589,
1.02348685082632E-16));
#12475=CARTESIAN_POINT('Ctrl Pts',(-0.121701328713853,0.118089450289423,
3.34304372375245E-17));
#12476=CARTESIAN_POINT('Ctrl Pts',(-0.127260382917516,0.110586827172589,
-2.01783277537669E-16));
#12477=CARTESIAN_POINT('Ctrl Pts',(-0.132096989238305,0.102614780608902,
-1.94343239418027E-16));
#12478=CARTESIAN_POINT('Ctrl Pts',(-0.13264315472071,0.101714550908896,
-1.94099397054962E-16));
#12479=CARTESIAN_POINT('Ctrl Pts',(-0.133180081100841,0.100808327459115,
-1.57928992210108E-16));
#12480=CARTESIAN_POINT('Ctrl Pts',(-0.13370774202371,0.0998962637199362,
-1.59594559789866E-16));
#12481=CARTESIAN_POINT('Ctrl Pts',(0.126907087985239,0.10793586530485,0.4));
#12482=CARTESIAN_POINT('Ctrl Pts',(0.135120918952682,0.100273232772223,
0.4));
#12483=CARTESIAN_POINT('Ctrl Pts',(0.142440334671421,0.0917705069751769,
0.4));
#12484=CARTESIAN_POINT('Ctrl Pts',(0.148860643047452,0.0826217448708272,
0.4));
#12485=CARTESIAN_POINT('Ctrl Pts',(0.153627635655713,0.0758289120703041,
0.4));
#12486=CARTESIAN_POINT('Ctrl Pts',(0.157898622411989,0.0686786359716775,
0.4));
#12487=CARTESIAN_POINT('Ctrl Pts',(0.161661540306914,0.0612359751068587,
0.4));
#12488=CARTESIAN_POINT('Ctrl Pts',(0.16388186285071,0.0568444076675918,
0.4));
#12489=CARTESIAN_POINT('Ctrl Pts',(0.165926693810491,0.0523458113179846,
0.4));
#12490=CARTESIAN_POINT('Ctrl Pts',(0.167781066520691,0.0477820314419273,
0.4));
#12491=CARTESIAN_POINT('Ctrl Pts',(0.172341633340749,0.0365580617608034,
0.4));
#12492=CARTESIAN_POINT('Ctrl Pts',(0.175769157493551,0.0249160193243555,
0.4));
#12493=CARTESIAN_POINT('Ctrl Pts',(0.178035263064282,0.013054133205507,
0.4));
#12494=CARTESIAN_POINT('Ctrl Pts',(0.179475094745571,0.00551736190307963,
0.4));
#12495=CARTESIAN_POINT('Ctrl Pts',(0.180445326972124,-0.00210904157496798,
0.4));
#12496=CARTESIAN_POINT('Ctrl Pts',(0.180929120151574,-0.00977934713136979,
0.4));
#12497=CARTESIAN_POINT('Ctrl Pts',(0.181154933194268,-0.0133595030939983,
0.4));
#12498=CARTESIAN_POINT('Ctrl Pts',(0.181274227458584,-0.0169457739644438,
0.4));
#12499=CARTESIAN_POINT('Ctrl Pts',(0.181285848432905,-0.020523365665851,
0.4));
#12500=CARTESIAN_POINT('Ctrl Pts',(0.181322136889233,-0.0316950003869775,
0.4));
#12501=CARTESIAN_POINT('Ctrl Pts',(0.180312890622882,-0.0428092364988491,
0.4));
#12502=CARTESIAN_POINT('Ctrl Pts',(0.178223999863926,-0.0537244994070254,
0.4));
#12503=CARTESIAN_POINT('Ctrl Pts',(0.177057515641768,-0.0598198310602051,
0.4));
#12504=CARTESIAN_POINT('Ctrl Pts',(0.175553812784148,-0.0658533566787336,
0.4));
#12505=CARTESIAN_POINT('Ctrl Pts',(0.173731861666353,-0.0718087245038544,
0.4));
#12506=CARTESIAN_POINT('Ctrl Pts',(0.172603795245643,-0.0754960080982815,
0.4));
#12507=CARTESIAN_POINT('Ctrl Pts',(0.171353052127964,-0.0791549057799955,
0.4));
#12508=CARTESIAN_POINT('Ctrl Pts',(0.169985341694702,-0.0827764782992071,
0.4));
#12509=CARTESIAN_POINT('Ctrl Pts',(0.165599957147556,-0.0943885767199536,
0.4));
#12510=CARTESIAN_POINT('Ctrl Pts',(0.16004703196815,-0.105538214993094,
0.4));
#12511=CARTESIAN_POINT('Ctrl Pts',(0.15349222199871,-0.116102682049509,
0.4));
#12512=CARTESIAN_POINT('Ctrl Pts',(0.14912551617891,-0.123140554999816,
0.4));
#12513=CARTESIAN_POINT('Ctrl Pts',(0.144312975580892,-0.129918879661908,
0.4));
#12514=CARTESIAN_POINT('Ctrl Pts',(0.139091822508928,-0.136399113069713,
0.4));
#12515=CARTESIAN_POINT('Ctrl Pts',(0.136383714422365,-0.139760281044032,
0.4));
#12516=CARTESIAN_POINT('Ctrl Pts',(0.133564151682456,-0.143042704899511,
0.4));
#12517=CARTESIAN_POINT('Ctrl Pts',(0.130641922795716,-0.146235745996435,
0.4));
#12518=CARTESIAN_POINT('Ctrl Pts',(0.124365895374187,-0.153093392765072,
0.4));
#12519=CARTESIAN_POINT('Ctrl Pts',(0.117640209417206,-0.159514676117615,
0.4));
#12520=CARTESIAN_POINT('Ctrl Pts',(0.110519094379635,-0.165448666244203,
0.4));
#12521=CARTESIAN_POINT('Ctrl Pts',(0.10626436178384,-0.16899411398399,0.4));
#12522=CARTESIAN_POINT('Ctrl Pts',(0.101868233565619,-0.172365528274035,
0.4));
#12523=CARTESIAN_POINT('Ctrl Pts',(0.0973404972469461,-0.175550904191779,
0.4));
#12524=CARTESIAN_POINT('Ctrl Pts',(0.0930576015741493,-0.178564028582011,
0.4));
#12525=CARTESIAN_POINT('Ctrl Pts',(0.0886627168583513,-0.181406366089281,
0.4));
#12526=CARTESIAN_POINT('Ctrl Pts',(0.0841711556372007,-0.184064773403165,
0.4));
#12527=CARTESIAN_POINT('Ctrl Pts',(0.0753868150238001,-0.189263935606354,
0.4));
#12528=CARTESIAN_POINT('Ctrl Pts',(0.066226257790498,-0.193765534094033,
0.4));
#12529=CARTESIAN_POINT('Ctrl Pts',(0.0567496916571122,-0.197494094154161,
0.4));
#12530=CARTESIAN_POINT('Ctrl Pts',(0.0555462198478251,-0.197967600787095,
0.4));
#12531=CARTESIAN_POINT('Ctrl Pts',(0.0543376370455851,-0.198428620952922,
0.4));
#12532=CARTESIAN_POINT('Ctrl Pts',(0.0531241180331689,-0.198877208092299,
0.4));
#12533=CARTESIAN_POINT('Ctrl Pts',(-0.166734374774229,-0.000128818837332453,
0.287148036339021));
#12534=CARTESIAN_POINT('Ctrl Pts',(-0.166805683280028,-0.00849491841283494,
0.287708823198405));
#12535=CARTESIAN_POINT('Ctrl Pts',(-0.166230437310337,-0.0168511701535723,
0.288269610057788));
#12536=CARTESIAN_POINT('Ctrl Pts',(-0.164974647650257,-0.0251038529149813,
0.288830396917172));
#12537=CARTESIAN_POINT('Ctrl Pts',(-0.156676448091865,-0.0796371960561269,
0.292536050353266));
#12538=CARTESIAN_POINT('Ctrl Pts',(-0.118662275502213,-0.12964819472467,
0.296241703789361));
#12539=CARTESIAN_POINT('Ctrl Pts',(-0.0683387086198173,-0.152238380008822,
0.299947357225455));
#12540=CARTESIAN_POINT('Ctrl Pts',(-0.0180151417374213,-0.174828565292974,
0.303653010661549));
#12541=CARTESIAN_POINT('Ctrl Pts',(0.0446178194377184,-0.169997937192735,
0.307358664097643));
#12542=CARTESIAN_POINT('Ctrl Pts',(0.0908810274585605,-0.139955915381198,
0.311064317533737));
#12543=CARTESIAN_POINT('Ctrl Pts',(0.137144235479403,-0.109913893569661,
0.314769970969832));
#12544=CARTESIAN_POINT('Ctrl Pts',(0.167037690345947,-0.0546604780468253,
0.318475624405926));
#12545=CARTESIAN_POINT('Ctrl Pts',(0.166873022942857,0.000499304166692509,
0.32218127784202));
#12546=CARTESIAN_POINT('Ctrl Pts',(0.166708355539768,0.0556590863802101,
0.325886931278115));
#12547=CARTESIAN_POINT('Ctrl Pts',(0.136485565867044,0.11072523528441,0.329592584714209));
#12548=CARTESIAN_POINT('Ctrl Pts',(0.0900441060064607,0.14049235813006,
0.333298238150303));
#12549=CARTESIAN_POINT('Ctrl Pts',(0.0436026461458773,0.17025948097571,
0.337003891586398));
#12550=CARTESIAN_POINT('Ctrl Pts',(-0.0190574839025661,0.17472757776281,
0.340709545022492));
#12551=CARTESIAN_POINT('Ctrl Pts',(-0.0692456664745192,0.151833326479749,
0.344415198458586));
#12552=CARTESIAN_POINT('Ctrl Pts',(-0.119433849046472,0.128939075196688,
0.34812085189468));
#12553=CARTESIAN_POINT('Ctrl Pts',(-0.157150084141935,0.0786824758434663,
0.351826505330774));
#12554=CARTESIAN_POINT('Ctrl Pts',(-0.165122125799463,0.0241090428979018,
0.355532158766869));
#12555=CARTESIAN_POINT('Ctrl Pts',(-0.166280881696888,0.0161766599544818,
0.356070784624253));
#12556=CARTESIAN_POINT('Ctrl Pts',(-0.166811221943148,0.00815307380534813,
0.356609410481637));
#12557=CARTESIAN_POINT('Ctrl Pts',(-0.166743774672904,0.000120896768023321,
0.357148036339021));
#12558=CARTESIAN_POINT('Ctrl Pts',(-0.0530170217188623,-0.198517432567172,
0.4));
#12559=CARTESIAN_POINT('Ctrl Pts',(-0.11904762702766,-0.180882981070921,
0.396294346563906));
#12560=CARTESIAN_POINT('Ctrl Pts',(-0.230986109789671,-0.0748521771817606,
0.388883039691718));
#12561=CARTESIAN_POINT('Ctrl Pts',(-0.188044707355364,0.153980890332211,
0.377766079383434));
#12562=CARTESIAN_POINT('Ctrl Pts',(0.0274206054315193,0.241260887402562,
0.366649119075152));
#12563=CARTESIAN_POINT('Ctrl Pts',(0.217614460633585,0.107865604001965,
0.355532158766869));
#12564=CARTESIAN_POINT('Ctrl Pts',(0.208602501412145,-0.124451281241526,
0.344415198458586));
#12565=CARTESIAN_POINT('Ctrl Pts',(0.00851095428263868,-0.242724098340208,
0.333298238150303));
#12566=CARTESIAN_POINT('Ctrl Pts',(-0.199352014072673,-0.138750852759731,
0.322181277842021));
#12567=CARTESIAN_POINT('Ctrl Pts',(-0.224662422339736,0.0923089884040401,
0.311064317533737));
#12568=CARTESIAN_POINT('Ctrl Pts',(-0.0442230349178335,0.238822732453524,
0.299947357225455));
#12569=CARTESIAN_POINT('Ctrl Pts',(0.176712068309585,0.166630571298318,
0.288830396917172));
#12570=CARTESIAN_POINT('Ctrl Pts',(0.235817802334529,-0.0581630255277868,
0.277713436608889));
#12571=CARTESIAN_POINT('Ctrl Pts',(0.078963123396891,-0.229690015875461,
0.266596476300606));
#12572=CARTESIAN_POINT('Ctrl Pts',(-0.150204697278654,-0.190870048415461,
0.255479515992324));
#12573=CARTESIAN_POINT('Ctrl Pts',(-0.241816852586086,0.0227471549627035,
0.24436255568404));
#12574=CARTESIAN_POINT('Ctrl Pts',(-0.111975498770539,0.215532531397883,
0.233245595375758));
#12575=CARTESIAN_POINT('Ctrl Pts',(0.120411794779082,0.210935552206459,
0.222128635067475));
#12576=CARTESIAN_POINT('Ctrl Pts',(0.242527242701154,0.0131659096813392,
0.211011674759192));
#12577=CARTESIAN_POINT('Ctrl Pts',(0.142538726865704,-0.196660905158453,
0.199894714450909));
#12578=CARTESIAN_POINT('Ctrl Pts',(-0.087985280286033,-0.226387709039377,
0.188777754142627));
#12579=CARTESIAN_POINT('Ctrl Pts',(-0.237933270688755,-0.0487909722550137,
0.177660793834344));
#12580=CARTESIAN_POINT('Ctrl Pts',(-0.169984441135179,0.173488023799692,
0.166543833526061));
#12581=CARTESIAN_POINT('Ctrl Pts',(0.0536344200204105,0.236888489580304,
0.155426873217778));
#12582=CARTESIAN_POINT('Ctrl Pts',(0.228135366692393,0.0833488984919273,
0.144309912909495));
#12583=CARTESIAN_POINT('Ctrl Pts',(0.193712423773769,-0.146520715699965,
0.133192952601213));
#12584=CARTESIAN_POINT('Ctrl Pts',(-0.0181106010581924,-0.24220824221319,
0.12207599229293));
#12585=CARTESIAN_POINT('Ctrl Pts',(-0.213347662204506,-0.116083820066942,
0.110959031984647));
#12586=CARTESIAN_POINT('Ctrl Pts',(-0.213204016359896,0.116348703664639,
0.0998420716763642));
#12587=CARTESIAN_POINT('Ctrl Pts',(-0.0178086481209368,0.24223078753445,
0.0887251113680815));
#12588=CARTESIAN_POINT('Ctrl Pts',(0.193892484656356,0.146279454291081,
0.0776081510597986));
#12589=CARTESIAN_POINT('Ctrl Pts',(0.228035008840565,-0.083631262664263,
0.0664911907515159));
#12590=CARTESIAN_POINT('Ctrl Pts',(0.0533337265757384,-0.236956827852518,
0.0553742304432329));
#12591=CARTESIAN_POINT('Ctrl Pts',(-0.170187709596901,-0.173273101663325,
0.0442572701349502));
#12592=CARTESIAN_POINT('Ctrl Pts',(-0.237895601007659,0.0490796089966686,
0.0331403098266674));
#12593=CARTESIAN_POINT('Ctrl Pts',(-0.0876598130547602,0.226510042114602,
0.0220233495183845));
#12594=CARTESIAN_POINT('Ctrl Pts',(0.142698384035228,0.196458332951895,
0.0109063892101018));
#12595=CARTESIAN_POINT('Ctrl Pts',(0.24267446543039,-0.0134175400107161,
-0.000210571098181212));
#12596=CARTESIAN_POINT('Ctrl Pts',(0.119815853924742,-0.211190891121989,
-0.0113275314064637));
#12597=CARTESIAN_POINT('Ctrl Pts',(-0.0343461939027931,-0.213802079752306,
-0.0187388382786524));
#12598=CARTESIAN_POINT('Ctrl Pts',(-0.0949553552261488,-0.182218155349229,
-0.0224444917147467));
#12599=CARTESIAN_POINT('Ctrl Pts',(-0.0496734897087706,-0.185997880000276,
0.407481497238249));
#12600=CARTESIAN_POINT('Ctrl Pts',(-0.111539858035973,-0.16947554968976,
0.403775843802155));
#12601=CARTESIAN_POINT('Ctrl Pts',(-0.216418911804395,-0.0701316055178259,
0.396364536929966));
#12602=CARTESIAN_POINT('Ctrl Pts',(-0.176185619877666,0.144270046171665,
0.385247576621683));
#12603=CARTESIAN_POINT('Ctrl Pts',(0.0256913179494246,0.226045707943951,
0.3741306163134));
#12604=CARTESIAN_POINT('Ctrl Pts',(0.203890549116156,0.101063032147195,
0.363013656005118));
#12605=CARTESIAN_POINT('Ctrl Pts',(0.195446931403795,-0.116602729417274,
0.351896695696835));
#12606=CARTESIAN_POINT('Ctrl Pts',(0.00797420877793362,-0.227416641110252,
0.340779735388552));
#12607=CARTESIAN_POINT('Ctrl Pts',(-0.186779828410061,-0.130000494806964,
0.329662775080269));
#12608=CARTESIAN_POINT('Ctrl Pts',(-0.210494029317946,0.0864874984836005,
0.318545814771986));
#12609=CARTESIAN_POINT('Ctrl Pts',(-0.0414340979304776,0.223761315859241,
0.307428854463704));
#12610=CARTESIAN_POINT('Ctrl Pts',(0.165567676606563,0.156121971778146,
0.29631189415542));
#12611=CARTESIAN_POINT('Ctrl Pts',(0.220945892425368,-0.0544949594736963,
0.285194933847139));
#12612=CARTESIAN_POINT('Ctrl Pts',(0.0739832938603632,-0.215204556383782,
0.274077973538855));
#12613=CARTESIAN_POINT('Ctrl Pts',(-0.140731999697103,-0.178832780082491,
0.262961013230573));
#12614=CARTESIAN_POINT('Ctrl Pts',(-0.226566611041236,0.0213125998275689,
0.251844052922289));
#12615=CARTESIAN_POINT('Ctrl Pts',(-0.104913735352921,0.201939917279227,
0.240727092614007));
#12616=CARTESIAN_POINT('Ctrl Pts',(0.112817994199877,0.197632847754131,
0.229610132305724));
#12617=CARTESIAN_POINT('Ctrl Pts',(0.227232200222333,0.0123355982259926,
0.218493171997441));
#12618=CARTESIAN_POINT('Ctrl Pts',(0.133549485665389,-0.184258434966565,
0.207376211689158));
#12619=CARTESIAN_POINT('Ctrl Pts',(-0.0824364661219098,-0.212110510371403,
0.196259251380876));
#12620=CARTESIAN_POINT('Ctrl Pts',(-0.22292794822775,-0.0457139571332818,
0.185142291072593));
#12621=CARTESIAN_POINT('Ctrl Pts',(-0.159264328957493,0.162546957286794,
0.17402533076431));
#12622=CARTESIAN_POINT('Ctrl Pts',(0.050251951628808,0.221949056506638,
0.162908370456027));
#12623=CARTESIAN_POINT('Ctrl Pts',(0.213747951548351,0.0780924789293308,
0.151791410147744));
#12624=CARTESIAN_POINT('Ctrl Pts',(0.181495900313161,-0.137280349357204,
0.140674449839462));
#12625=CARTESIAN_POINT('Ctrl Pts',(-0.0169684513787713,-0.226933317581584,
0.129557489531179));
#12626=CARTESIAN_POINT('Ctrl Pts',(-0.199892837419333,-0.108762964317901,
0.118440529222896));
#12627=CARTESIAN_POINT('Ctrl Pts',(-0.199758250636587,0.109011142963884,
0.107323568914613));
#12628=CARTESIAN_POINT('Ctrl Pts',(-0.0166855411805929,0.226954441076403,
0.0962066086063302));
#12629=CARTESIAN_POINT('Ctrl Pts',(0.181664605610217,0.137054303160666,
0.0850896482980475));
#12630=CARTESIAN_POINT('Ctrl Pts',(0.213653922790069,-0.0783570357330495,
0.0739726879897647));
#12631=CARTESIAN_POINT('Ctrl Pts',(0.0499702214929919,-0.222013085008269,
0.0628557276814818));
#12632=CARTESIAN_POINT('Ctrl Pts',(-0.159454778241781,-0.162345589269827,
0.0517387673731991));
#12633=CARTESIAN_POINT('Ctrl Pts',(-0.222892654194709,0.0459843909251343,
0.0406218070649163));
#12634=CARTESIAN_POINT('Ctrl Pts',(-0.0821315245646701,0.212225128480008,
0.0295048467566334));
#12635=CARTESIAN_POINT('Ctrl Pts',(0.133699074014756,0.18406863802793,0.0183878864483507));
#12636=CARTESIAN_POINT('Ctrl Pts',(0.227370138312564,-0.0125713594244052,
0.00727092614006769));
#12637=CARTESIAN_POINT('Ctrl Pts',(0.112259636507661,-0.197872083655765,
-0.00384603416821484));
#12638=CARTESIAN_POINT('Ctrl Pts',(-0.0321801424156356,-0.200318597008467,
-0.0112573410404035));
#12639=CARTESIAN_POINT('Ctrl Pts',(-0.0889669715064481,-0.170726520861333,
-0.0149629944764978));
#12640=CARTESIAN_POINT('Ctrl Pts',(-0.0463299576986789,-0.17347832743338,
0.414962994476498));
#12641=CARTESIAN_POINT('Ctrl Pts',(-0.104032089044287,-0.158068118308599,
0.411257341040404));
#12642=CARTESIAN_POINT('Ctrl Pts',(-0.201851713819119,-0.0654110338538912,
0.403846034168215));
#12643=CARTESIAN_POINT('Ctrl Pts',(-0.164326532399969,0.134559202011118,
0.392729073859932));
#12644=CARTESIAN_POINT('Ctrl Pts',(0.0239620304673297,0.210830528485339,
0.38161211355165));
#12645=CARTESIAN_POINT('Ctrl Pts',(0.190166637598728,0.0942604602924253,
0.370495153243366));
#12646=CARTESIAN_POINT('Ctrl Pts',(0.182291361395445,-0.108754177593023,
0.359378192935084));
#12647=CARTESIAN_POINT('Ctrl Pts',(0.00743746327322925,-0.212109183880296,
0.348261232626801));
#12648=CARTESIAN_POINT('Ctrl Pts',(-0.17420764274745,-0.121250136854196,
0.337144272318518));
#12649=CARTESIAN_POINT('Ctrl Pts',(-0.196325636296155,0.0806660085631606,
0.326027312010236));
#12650=CARTESIAN_POINT('Ctrl Pts',(-0.0386451609431219,0.208699899264959,
0.314910351701952));
#12651=CARTESIAN_POINT('Ctrl Pts',(0.154423284903542,0.145613372257974,
0.30379339139367));
#12652=CARTESIAN_POINT('Ctrl Pts',(0.206073982516206,-0.0508268934196057,
0.292676431085387));
#12653=CARTESIAN_POINT('Ctrl Pts',(0.0690034643238352,-0.200719096892102,
0.281559470777104));
#12654=CARTESIAN_POINT('Ctrl Pts',(-0.131259302115551,-0.166795511749521,
0.270442510468821));
#12655=CARTESIAN_POINT('Ctrl Pts',(-0.211316369496387,0.0198780446924348,
0.259325550160539));
#12656=CARTESIAN_POINT('Ctrl Pts',(-0.097851971935304,0.188347303160571,
0.248208589852256));
#12657=CARTESIAN_POINT('Ctrl Pts',(0.105224193620671,0.184330143301803,
0.237091629543973));
#12658=CARTESIAN_POINT('Ctrl Pts',(0.211937157743512,0.0115052867706461,
0.22597466923569));
#12659=CARTESIAN_POINT('Ctrl Pts',(0.124560244465074,-0.171855964774677,
0.214857708927407));
#12660=CARTESIAN_POINT('Ctrl Pts',(-0.0768876519577869,-0.197833311703429,
0.203740748619125));
#12661=CARTESIAN_POINT('Ctrl Pts',(-0.207922625766744,-0.0426369420115498,
0.192623788310841));
#12662=CARTESIAN_POINT('Ctrl Pts',(-0.148544216779807,0.151605890773896,
0.181506828002559));
#12663=CARTESIAN_POINT('Ctrl Pts',(0.0468694832372058,0.207009623432973,
0.170389867694276));
#12664=CARTESIAN_POINT('Ctrl Pts',(0.199360536404307,0.0728360593667339,
0.159272907385993));
#12665=CARTESIAN_POINT('Ctrl Pts',(0.169279376852553,-0.128039983014444,
0.148155947077711));
#12666=CARTESIAN_POINT('Ctrl Pts',(-0.0158263016993501,-0.211658392949978,
0.137038986769427));
#12667=CARTESIAN_POINT('Ctrl Pts',(-0.18643801263416,-0.101442108568861,
0.125922026461145));
#12668=CARTESIAN_POINT('Ctrl Pts',(-0.186312484913278,0.101673582263129,
0.114805066152862));
#12669=CARTESIAN_POINT('Ctrl Pts',(-0.0155624342402491,0.211678094618356,
0.103688105844579));
#12670=CARTESIAN_POINT('Ctrl Pts',(0.169436726564079,0.127829152030252,
0.0925711455362964));
#12671=CARTESIAN_POINT('Ctrl Pts',(0.199272836739573,-0.0730828088018361,
0.0814541852280136));
#12672=CARTESIAN_POINT('Ctrl Pts',(0.0466067164102457,-0.207069342164019,
0.0703372249197308));
#12673=CARTESIAN_POINT('Ctrl Pts',(-0.148721846886662,-0.15141807687633,
0.0592202646114479));
#12674=CARTESIAN_POINT('Ctrl Pts',(-0.207889707381759,0.0428891728536002,
0.0481033043031653));
#12675=CARTESIAN_POINT('Ctrl Pts',(-0.07660323607458,0.197940214845413,
0.0369863439948823));
#12676=CARTESIAN_POINT('Ctrl Pts',(0.124699763994284,0.171678943103966,
0.0258693836865997));
#12677=CARTESIAN_POINT('Ctrl Pts',(0.212065811194736,-0.0117251788380946,
0.0147524233783166));
#12678=CARTESIAN_POINT('Ctrl Pts',(0.10470341909058,-0.184553276189541,
0.00363546307003411));
#12679=CARTESIAN_POINT('Ctrl Pts',(-0.030014090928478,-0.186835114264629,
-0.00377584380215461));
#12680=CARTESIAN_POINT('Ctrl Pts',(-0.0829785877867473,-0.159234886373437,
-0.00748149723824889));
#12681=CARTESIAN_POINT('Ctrl Pts',(-0.0429864256885872,-0.160958774866484,
0.422444491714747));
#12682=CARTESIAN_POINT('Ctrl Pts',(-0.0965243200526006,-0.146660686927438,
0.418738838278652));
#12683=CARTESIAN_POINT('Ctrl Pts',(-0.187284515833844,-0.0606904621899564,
0.411327531406464));
#12684=CARTESIAN_POINT('Ctrl Pts',(-0.152467444922271,0.124848357850572,
0.400210571098181));
#12685=CARTESIAN_POINT('Ctrl Pts',(0.0222327429852349,0.195615349026728,
0.389093610789898));
#12686=CARTESIAN_POINT('Ctrl Pts',(0.1764427260813,0.0874578884376555,0.377976650481615));
#12687=CARTESIAN_POINT('Ctrl Pts',(0.169135791387095,-0.100905625768771,
0.366859690173333));
#12688=CARTESIAN_POINT('Ctrl Pts',(0.00690071776852435,-0.19680172665034,
0.35574272986505));
#12689=CARTESIAN_POINT('Ctrl Pts',(-0.161635457084839,-0.112499778901429,
0.344625769556767));
#12690=CARTESIAN_POINT('Ctrl Pts',(-0.182157243274365,0.0748445186427209,
0.333508809248484));
#12691=CARTESIAN_POINT('Ctrl Pts',(-0.035856223955766,0.193638482670676,
0.322391848940201));
#12692=CARTESIAN_POINT('Ctrl Pts',(0.14327889320052,0.135104772737801,0.311274888631918));
#12693=CARTESIAN_POINT('Ctrl Pts',(0.191202072607045,-0.0471588273655153,
0.300157928323636));
#12694=CARTESIAN_POINT('Ctrl Pts',(0.0640236347873075,-0.186233637400423,
0.289040968015352));
#12695=CARTESIAN_POINT('Ctrl Pts',(-0.121786604534,-0.154758243416551,0.277924007707071));
#12696=CARTESIAN_POINT('Ctrl Pts',(-0.196066127951537,0.0184434895573008,
0.266807047398787));
#12697=CARTESIAN_POINT('Ctrl Pts',(-0.090790208517687,0.174754689041914,
0.255690087090505));
#12698=CARTESIAN_POINT('Ctrl Pts',(0.0976303930414654,0.171027438849476,
0.244573126782221));
#12699=CARTESIAN_POINT('Ctrl Pts',(0.196642115264691,0.0106749753152992,
0.233456166473939));
#12700=CARTESIAN_POINT('Ctrl Pts',(0.115571003264759,-0.159453494582788,
0.222339206165656));
#12701=CARTESIAN_POINT('Ctrl Pts',(-0.0713388377936639,-0.183556113035455,
0.211222245857374));
#12702=CARTESIAN_POINT('Ctrl Pts',(-0.192917303305739,-0.0395599268898177,
0.20010528554909));
#12703=CARTESIAN_POINT('Ctrl Pts',(-0.137824104602121,0.140664824260998,
0.188988325240808));
#12704=CARTESIAN_POINT('Ctrl Pts',(0.0434870148456035,0.192070190359307,
0.177871364932525));
#12705=CARTESIAN_POINT('Ctrl Pts',(0.184973121260264,0.0675796398041375,
0.166754404624242));
#12706=CARTESIAN_POINT('Ctrl Pts',(0.157062853391945,-0.118799616671684,
0.155637444315959));
#12707=CARTESIAN_POINT('Ctrl Pts',(-0.0146841520199287,-0.196383468318372,
0.144520484007676));
#12708=CARTESIAN_POINT('Ctrl Pts',(-0.172983187848988,-0.0941212528198204,
0.133403523699394));
#12709=CARTESIAN_POINT('Ctrl Pts',(-0.172866719189968,0.0943360215623745,
0.122286563391111));
#12710=CARTESIAN_POINT('Ctrl Pts',(-0.0144393272999055,0.196401748160308,
0.111169603082828));
#12711=CARTESIAN_POINT('Ctrl Pts',(0.157208847517941,0.118604000899837,
0.100052642774545));
#12712=CARTESIAN_POINT('Ctrl Pts',(0.184891750689077,-0.0678085818706227,
0.0889356824662626));
#12713=CARTESIAN_POINT('Ctrl Pts',(0.0432432113274997,-0.192125599319769,
0.0778187221579795));
#12714=CARTESIAN_POINT('Ctrl Pts',(-0.137988915531543,-0.140490564482832,
0.0667017618496969));
#12715=CARTESIAN_POINT('Ctrl Pts',(-0.192886760568809,0.039793954782066,
0.0555848015414141));
#12716=CARTESIAN_POINT('Ctrl Pts',(-0.0710749475844899,0.183655301210818,
0.0444678412331312));
#12717=CARTESIAN_POINT('Ctrl Pts',(0.115700453973812,0.159289248180001,
0.0333508809248486));
#12718=CARTESIAN_POINT('Ctrl Pts',(0.19676148407691,-0.0108789982517839,
0.0222339206165655));
#12719=CARTESIAN_POINT('Ctrl Pts',(0.0971472016734982,-0.171234468723317,
0.011116960308283));
#12720=CARTESIAN_POINT('Ctrl Pts',(-0.0278480394413205,-0.17335163152079,
0.00370565343609428));
#12721=CARTESIAN_POINT('Ctrl Pts',(-0.0769902040670466,-0.147743251885541,
0.));
#12722=CARTESIAN_POINT('Ctrl Pts',(-0.0769902040670466,-0.147743251885541,
0.));
#12723=CARTESIAN_POINT('Ctrl Pts',(-0.0676919232950484,-0.154046060403006,
-1.40302012364989E-17));
#12724=CARTESIAN_POINT('Ctrl Pts',(-0.0577736401959485,-0.159289942754579,
-5.08211119036949E-18));
#12725=CARTESIAN_POINT('Ctrl Pts',(-0.0474255897387057,-0.163513503780882,
-6.24500451351651E-17));
#12726=CARTESIAN_POINT('Ctrl Pts',(-0.0397423269274568,-0.16664943063962,
-1.05044823277914E-16));
#12727=CARTESIAN_POINT('Ctrl Pts',(-0.0318209566230111,-0.169222252731152,
-2.46304152627642E-17));
#12728=CARTESIAN_POINT('Ctrl Pts',(-0.0237275895471058,-0.17123468536678,
-2.77555756156289E-17));
#12729=CARTESIAN_POINT('Ctrl Pts',(-0.0189520706408748,-0.172422128121918,
-2.9599587163621E-17));
#12730=CARTESIAN_POINT('Ctrl Pts',(-0.0141112573217385,-0.17341466403244,
-4.4351679547558E-17));
#12731=CARTESIAN_POINT('Ctrl Pts',(-0.00924927591576842,-0.174207012929982,
-2.77555756156289E-17));
#12732=CARTESIAN_POINT('Ctrl Pts',(0.00270810149489128,-0.176155686529844,
1.30602691378976E-17));
#12733=CARTESIAN_POINT('Ctrl Pts',(0.0148209433822563,-0.176906695131537,
1.46993562916598E-16));
#12734=CARTESIAN_POINT('Ctrl Pts',(0.0268896779998609,-0.176476481527875,
2.70616862252382E-16));
#12735=CARTESIAN_POINT('Ctrl Pts',(0.0345578784611946,-0.176203133554073,
3.49164304965678E-16));
#12736=CARTESIAN_POINT('Ctrl Pts',(0.0422089684879974,-0.175452013432818,
9.66603464943305E-17));
#12737=CARTESIAN_POINT('Ctrl Pts',(0.0497946177189777,-0.174216878926306,
8.32667268468867E-17));
#12738=CARTESIAN_POINT('Ctrl Pts',(0.0533352666340748,-0.173640372220377,
7.70151716497034E-17));
#12739=CARTESIAN_POINT('Ctrl Pts',(0.0568581744479369,-0.172958655817438,
1.70258089114663E-16));
#12740=CARTESIAN_POINT('Ctrl Pts',(0.060348661217807,-0.172173896054275,
1.78676518025611E-16));
#12741=CARTESIAN_POINT('Ctrl Pts',(0.0712482444786328,-0.169723362663869,
2.04964360636066E-16));
#12742=CARTESIAN_POINT('Ctrl Pts',(0.0818592181722872,-0.166266280890076,
6.45230284175388E-17));
#12743=CARTESIAN_POINT('Ctrl Pts',(0.0920359693799999,-0.161800897340594,
8.32667268468867E-17));
#12744=CARTESIAN_POINT('Ctrl Pts',(0.0977189075830844,-0.15930732171446,
9.2085789653526E-17));
#12745=CARTESIAN_POINT('Ctrl Pts',(0.103266552483982,-0.156498733846781,
1.36090193073051E-16));
#12746=CARTESIAN_POINT('Ctrl Pts',(0.10866718341613,-0.153397267387788,
1.35308431126191E-16));
#12747=CARTESIAN_POINT('Ctrl Pts',(0.11201100284804,-0.151476983638854,
1.34824400496829E-16));
#12748=CARTESIAN_POINT('Ctrl Pts',(0.115299850264095,-0.149443414758961,
6.72250876644913E-17));
#12749=CARTESIAN_POINT('Ctrl Pts',(0.118526280975827,-0.147304116216612,
7.45931094670027E-17));
#12750=CARTESIAN_POINT('Ctrl Pts',(0.128871394179061,-0.140444745111681,
9.82176737118538E-17));
#12751=CARTESIAN_POINT('Ctrl Pts',(0.138505844759193,-0.132550010250448,
1.65756112205145E-16));
#12752=CARTESIAN_POINT('Ctrl Pts',(0.147346858840741,-0.123808721893542,
1.51788304147971E-16));
#12753=CARTESIAN_POINT('Ctrl Pts',(0.153236584111842,-0.117985432114476,
1.42483200532319E-16));
#12754=CARTESIAN_POINT('Ctrl Pts',(0.158774063957949,-0.111785241608361,
1.64345680573043E-16));
#12755=CARTESIAN_POINT('Ctrl Pts',(0.163930004359885,-0.10525301636718,
1.83013326715553E-16));
#12756=CARTESIAN_POINT('Ctrl Pts',(0.166604294556271,-0.101864872874187,
1.92695886864967E-16));
#12757=CARTESIAN_POINT('Ctrl Pts',(0.169177014089436,-0.0983855914277328,
9.88896432374603E-17));
#12758=CARTESIAN_POINT('Ctrl Pts',(0.171639746961675,-0.0948261071091421,
6.33174068731535E-17));
#12759=CARTESIAN_POINT('Ctrl Pts',(0.176928913626705,-0.087181467280431,
-1.30804391537608E-17));
#12760=CARTESIAN_POINT('Ctrl Pts',(0.181692601485159,-0.0791955439239232,
1.01225052450567E-16));
#12761=CARTESIAN_POINT('Ctrl Pts',(0.185893224525176,-0.0709325403972633,
7.80625564189563E-17));
#12762=CARTESIAN_POINT('Ctrl Pts',(0.188402594077904,-0.065996384673136,
6.42257370345008E-17));
#12763=CARTESIAN_POINT('Ctrl Pts',(0.190710898758921,-0.0609611385701718,
-2.50862304223578E-17));
#12764=CARTESIAN_POINT('Ctrl Pts',(0.192808617454456,-0.0558390095854279,
8.67361737988404E-19));
#12765=CARTESIAN_POINT('Ctrl Pts',(0.194793596006727,-0.0509921651546984,
2.54260997148077E-17));
#12766=CARTESIAN_POINT('Ctrl Pts',(0.196587084810493,-0.0460741094242064,
1.76166452828751E-16));
#12767=CARTESIAN_POINT('Ctrl Pts',(0.198179668914476,-0.0411027133746267,
1.06251812903579E-16));
#12768=CARTESIAN_POINT('Ctrl Pts',(0.201293818615582,-0.0313816120003518,
-3.0459745676829E-17));
#12769=CARTESIAN_POINT('Ctrl Pts',(0.203644165628124,-0.0214489479791743,
-7.88851781500756E-17));
#12770=CARTESIAN_POINT('Ctrl Pts',(0.205170522984607,-0.0113802171361653,
-8.38359329874416E-17));
#12771=CARTESIAN_POINT('Ctrl Pts',(0.205364360570336,-0.0101015529559362,
-8.50972051141002E-17));
#12772=CARTESIAN_POINT('Ctrl Pts',(0.205544887409679,-0.00882068448784814,
-9.83390714117784E-17));
#12773=CARTESIAN_POINT('Ctrl Pts',(0.205712194497466,-0.00753777023904148,
-9.71445146547012E-17));
#12774=CARTESIAN_POINT('Ctrl Pts',(-0.166378928688253,9.26016813348553E-5,
0.337851963660979));
#12775=CARTESIAN_POINT('Ctrl Pts',(-0.166489498819458,0.0218084776863281,
0.336404245523481));
#12776=CARTESIAN_POINT('Ctrl Pts',(-0.162543310453018,0.0434858705291553,
0.334956527385983));
#12777=CARTESIAN_POINT('Ctrl Pts',(-0.154353442356344,0.0634194630566879,
0.333508809248484));
#12778=CARTESIAN_POINT('Ctrl Pts',(-0.133390236834832,0.114442506652039,
0.32980315581239));
#12779=CARTESIAN_POINT('Ctrl Pts',(-0.0846232303952993,0.154040494661357,
0.326097502376296));
#12780=CARTESIAN_POINT('Ctrl Pts',(-0.0303838743161517,0.164083870343871,
0.322391848940201));
#12781=CARTESIAN_POINT('Ctrl Pts',(0.0238554817629959,0.174127246026385,
0.318686195504107));
#12782=CARTESIAN_POINT('Ctrl Pts',(0.083567187481758,0.154616009382093,
0.314980542068013));
#12783=CARTESIAN_POINT('Ctrl Pts',(0.121410236908893,0.114483124376061,
0.311274888631919));
#12784=CARTESIAN_POINT('Ctrl Pts',(0.159253286336028,0.0743502393700291,
0.307569235195824));
#12785=CARTESIAN_POINT('Ctrl Pts',(0.175227679471537,0.0135957060022568,
0.30386358175973));
#12786=CARTESIAN_POINT('Ctrl Pts',(0.162018469736001,-0.0399606956874471,
0.300157928323636));
#12787=CARTESIAN_POINT('Ctrl Pts',(0.148809260000466,-0.0935170973771512,
0.296452274887542));
#12788=CARTESIAN_POINT('Ctrl Pts',(0.106416447393887,-0.139875367388787,
0.292746621451447));
#12789=CARTESIAN_POINT('Ctrl Pts',(0.0542516678703787,-0.157808603397293,
0.289040968015353));
#12790=CARTESIAN_POINT('Ctrl Pts',(0.00208688834687113,-0.175741839405799,
0.285335314579258));
#12791=CARTESIAN_POINT('Ctrl Pts',(-0.0598498580935646,-0.165250041411175,
0.281629661143165));
#12792=CARTESIAN_POINT('Ctrl Pts',(-0.103198151883372,-0.131137186918221,
0.27792400770707));
#12793=CARTESIAN_POINT('Ctrl Pts',(-0.142472010228314,-0.100230701380539,
0.274566659691707));
#12794=CARTESIAN_POINT('Ctrl Pts',(-0.166487561106675,-0.0499349019762822,
0.271209311676343));
#12795=CARTESIAN_POINT('Ctrl Pts',(-0.166813199754551,8.97901853038408E-5,
0.267851963660979));
#12796=CARTESIAN_POINT('Ctrl Pts',(-0.0530170217188623,-0.198517432567172,
0.4));
#12797=CARTESIAN_POINT('Ctrl Pts',(-0.0654220238783876,-0.193924320176499,
0.4));
#12798=CARTESIAN_POINT('Ctrl Pts',(-0.077272885559963,-0.188065277791306,
0.4));
#12799=CARTESIAN_POINT('Ctrl Pts',(-0.088451754807208,-0.181103168839745,
0.4));
#12800=CARTESIAN_POINT('Ctrl Pts',(-0.0941395501466508,-0.177560856109221,
0.4));
#12801=CARTESIAN_POINT('Ctrl Pts',(-0.0996529437908355,-0.17373223440453,
0.4));
#12802=CARTESIAN_POINT('Ctrl Pts',(-0.104972932012442,-0.169635136338519,
0.4));
#12803=CARTESIAN_POINT('Ctrl Pts',(-0.108688724528218,-0.166773482196456,
0.4));
#12804=CARTESIAN_POINT('Ctrl Pts',(-0.112310113490456,-0.163780806587061,
0.4));
#12805=CARTESIAN_POINT('Ctrl Pts',(-0.115829752094829,-0.160662744842601,
0.4));
#12806=CARTESIAN_POINT('Ctrl Pts',(-0.118823489359745,-0.158010581172415,
0.4));
#12807=CARTESIAN_POINT('Ctrl Pts',(-0.121744082040539,-0.15526683742813,
0.4));
#12808=CARTESIAN_POINT('Ctrl Pts',(-0.124575376453565,-0.152447107362845,
0.4));
#12809=CARTESIAN_POINT('Ctrl Pts',(-0.13372228318865,-0.14333756092832,
0.4));
#12810=CARTESIAN_POINT('Ctrl Pts',(-0.141972119474717,-0.133410188786047,
0.4));
#12811=CARTESIAN_POINT('Ctrl Pts',(-0.14918937059335,-0.122798683211669,
0.4));
#12812=CARTESIAN_POINT('Ctrl Pts',(-0.153996665370339,-0.115730530187037,
0.4));
#12813=CARTESIAN_POINT('Ctrl Pts',(-0.158345026572386,-0.108358186354888,
0.4));
#12814=CARTESIAN_POINT('Ctrl Pts',(-0.162181700444826,-0.100717710946895,
0.4));
#12815=CARTESIAN_POINT('Ctrl Pts',(-0.163843640896044,-0.0974080694268549,
0.4));
#12816=CARTESIAN_POINT('Ctrl Pts',(-0.165409068660182,-0.0940481991896131,
0.4));
#12817=CARTESIAN_POINT('Ctrl Pts',(-0.16686835322227,-0.0906540285733807,
0.4));
#12818=CARTESIAN_POINT('Ctrl Pts',(-0.171500933618561,-0.0798790442646778,
0.4));
#12819=CARTESIAN_POINT('Ctrl Pts',(-0.175084020385089,-0.0687267134060537,
0.4));
#12820=CARTESIAN_POINT('Ctrl Pts',(-0.177491918105115,-0.0572965665658765,
0.4));
#12821=CARTESIAN_POINT('Ctrl Pts',(-0.179346683049952,-0.0484921080138423,
0.4));
#12822=CARTESIAN_POINT('Ctrl Pts',(-0.180503025417496,-0.0395222674034557,
0.4));
#12823=CARTESIAN_POINT('Ctrl Pts',(-0.180973680426704,-0.0304659686022641,
0.4));
#12824=CARTESIAN_POINT('Ctrl Pts',(-0.181157610795637,-0.0269267979845529,
0.4));
#12825=CARTESIAN_POINT('Ctrl Pts',(-0.181236344221217,-0.0233770431725763,
0.4));
#12826=CARTESIAN_POINT('Ctrl Pts',(-0.181211258491791,-0.0198321075205306,
0.4));
#12827=CARTESIAN_POINT('Ctrl Pts',(-0.181128976637152,-0.00820462501560692,
0.4));
#12828=CARTESIAN_POINT('Ctrl Pts',(-0.179934875816279,0.00340488210138015,
0.4));
#12829=CARTESIAN_POINT('Ctrl Pts',(-0.177672440840337,0.0148269863576212,
0.4));
#12830=CARTESIAN_POINT('Ctrl Pts',(-0.176391160190413,0.0212956457094027,
0.4));
#12831=CARTESIAN_POINT('Ctrl Pts',(-0.174766470591578,0.0277040200840655,
0.4));
#12832=CARTESIAN_POINT('Ctrl Pts',(-0.172801022035689,0.0340181492506376,
0.4));
#12833=CARTESIAN_POINT('Ctrl Pts',(-0.171289396872808,0.0388743417473916,
0.4));
#12834=CARTESIAN_POINT('Ctrl Pts',(-0.169574623865183,0.0436773188170338,
0.4));
#12835=CARTESIAN_POINT('Ctrl Pts',(-0.167666912323756,0.0483881533931519,
0.4));
#12836=CARTESIAN_POINT('Ctrl Pts',(-0.164214525512166,0.0569133537753892,
0.4));
#12837=CARTESIAN_POINT('Ctrl Pts',(-0.160126908536967,0.0651538844249133,
0.4));
#12838=CARTESIAN_POINT('Ctrl Pts',(-0.15541346823496,0.0730140785601572,
0.4));
#12839=CARTESIAN_POINT('Ctrl Pts',(-0.152992964434853,0.0770505420676795,
0.4));
#12840=CARTESIAN_POINT('Ctrl Pts',(-0.150406465661651,0.0809868395219411,
0.4));
#12841=CARTESIAN_POINT('Ctrl Pts',(-0.147664107811223,0.0847961900136081,
0.4));
#12842=CARTESIAN_POINT('Ctrl Pts',(-0.142209781496364,0.092372677752427,
0.4));
#12843=CARTESIAN_POINT('Ctrl Pts',(-0.13613226485763,0.0994618610044957,
0.4));
#12844=CARTESIAN_POINT('Ctrl Pts',(-0.129436334451722,0.105951160758884,
0.4));
#12845=CARTESIAN_POINT('Ctrl Pts',(-0.128680208499678,0.106683953314577,
0.4));
#12846=CARTESIAN_POINT('Ctrl Pts',(-0.127916183191217,0.107409072087309,
0.4));
#12847=CARTESIAN_POINT('Ctrl Pts',(-0.127144402274346,0.108126457236474,
0.4));
#12848=CARTESIAN_POINT('Origin',(0.,0.,0.4));
#12849=CARTESIAN_POINT('',(0.202072594216369,-0.35,0.4));
#12850=CARTESIAN_POINT('',(0.404145188432738,0.,0.4));
#12851=CARTESIAN_POINT('',(0.202072594216369,-0.35,0.4));
#12852=CARTESIAN_POINT('',(0.202072594216369,0.35,0.4));
#12853=CARTESIAN_POINT('',(0.404145188432738,0.,0.4));
#12854=CARTESIAN_POINT('',(-0.202072594216369,0.35,0.4));
#12855=CARTESIAN_POINT('',(0.202072594216369,0.35,0.4));
#12856=CARTESIAN_POINT('',(-0.404145188432738,5.55111512312578E-17,0.4));
#12857=CARTESIAN_POINT('',(-0.202072594216369,0.35,0.4));
#12858=CARTESIAN_POINT('',(-0.202072594216369,-0.35,0.4));
#12859=CARTESIAN_POINT('',(-0.404145188432738,4.94935111404957E-17,0.4));
#12860=CARTESIAN_POINT('',(-0.202072594216369,-0.35,0.4));
#12861=CARTESIAN_POINT('Origin',(0.,0.,0.2));
#12862=CARTESIAN_POINT('Origin',(-0.202072594216369,-0.35,0.));
#12863=CARTESIAN_POINT('',(-0.202072594216369,-0.35,0.));
#12864=CARTESIAN_POINT('',(0.202072594216369,-0.35,0.));
#12865=CARTESIAN_POINT('',(-0.202072594216369,-0.35,0.));
#12866=CARTESIAN_POINT('',(0.202072594216369,-0.35,0.));
#12867=CARTESIAN_POINT('',(-0.202072594216369,-0.35,0.));
#12868=CARTESIAN_POINT('Origin',(-0.404145188432738,4.94935111404957E-17,
0.));
#12869=CARTESIAN_POINT('',(-0.404145188432738,4.94935111404957E-17,0.));
#12870=CARTESIAN_POINT('',(-0.404145188432738,4.94935111404957E-17,0.));
#12871=CARTESIAN_POINT('',(-0.404145188432738,4.94935111404957E-17,0.));
#12872=CARTESIAN_POINT('Origin',(-0.202072594216369,0.35,0.));
#12873=CARTESIAN_POINT('',(-0.202072594216369,0.35,0.));
#12874=CARTESIAN_POINT('',(-0.202072594216369,0.35,0.));
#12875=CARTESIAN_POINT('',(-0.202072594216369,0.35,0.));
#12876=CARTESIAN_POINT('Origin',(0.202072594216369,0.35,0.));
#12877=CARTESIAN_POINT('',(0.202072594216369,0.35,0.));
#12878=CARTESIAN_POINT('',(0.202072594216369,0.35,0.));
#12879=CARTESIAN_POINT('',(0.202072594216369,0.35,0.));
#12880=CARTESIAN_POINT('Origin',(0.404145188432738,0.,0.));
#12881=CARTESIAN_POINT('',(0.404145188432738,0.,0.));
#12882=CARTESIAN_POINT('',(0.404145188432738,0.,0.));
#12883=CARTESIAN_POINT('',(0.404145188432738,0.,0.));
#12884=CARTESIAN_POINT('Origin',(0.202072594216369,-0.35,0.));
#12885=CARTESIAN_POINT('',(0.202072594216369,-0.35,0.));
#12886=CARTESIAN_POINT('Origin',(0.,0.,0.));
#12947=UNCERTAINTY_MEASURE_WITH_UNIT(LENGTH_MEASURE(0.001),#12964,
'DISTANCE_ACCURACY_VALUE',
'Maximum model space distance between geometric entities at asserted c
onnectivities');
#12949=UNCERTAINTY_MEASURE_WITH_UNIT(LENGTH_MEASURE(0.001),#12964,
'DISTANCE_ACCURACY_VALUE',
'Maximum model space distance between geometric entities at asserted c
onnectivities');
#12961=(
GEOMETRIC_REPRESENTATION_CONTEXT(3)
GLOBAL_UNCERTAINTY_ASSIGNED_CONTEXT((#12947))
GLOBAL_UNIT_ASSIGNED_CONTEXT((#12964,#12966,#12967))
REPRESENTATION_CONTEXT('','3D')
);
#12963=(
GEOMETRIC_REPRESENTATION_CONTEXT(3)
GLOBAL_UNCERTAINTY_ASSIGNED_CONTEXT((#12949))
GLOBAL_UNIT_ASSIGNED_CONTEXT((#12964,#12966,#12967))
REPRESENTATION_CONTEXT('','3D')
);
#12964=(
LENGTH_UNIT()
NAMED_UNIT(*)
SI_UNIT(.CENTI.,.METRE.)
);
#12966=(
NAMED_UNIT(*)
PLANE_ANGLE_UNIT()
SI_UNIT($,.RADIAN.)
);
#12967=(
NAMED_UNIT(*)
SI_UNIT($,.STERADIAN.)
SOLID_ANGLE_UNIT()
);
#12979=SHAPE_DEFINITION_REPRESENTATION(#12992,#13045);
#12992=PRODUCT_DEFINITION_SHAPE('',$,#13059);
#13045=SHAPE_REPRESENTATION('',(#5267),#12961);
#13047=PRODUCT_DEFINITION_CONTEXT('part definition',#13088,'design');
#13059=PRODUCT_DEFINITION('Hex nut M4','Hex nut M4',#13072,#13047);
#13072=PRODUCT_DEFINITION_FORMATION('',$,#13101);
#13088=APPLICATION_CONTEXT(
'Core Data for Automotive Mechanical Design Process');
#13089=PRODUCT_CONTEXT('part definition',#13088,'mechanical');
#13101=PRODUCT('Hex nut M4','Hex nut M4',$,(#13089));
#13114=PRESENTATION_STYLE_ASSIGNMENT((#13127));
#13127=SURFACE_STYLE_USAGE(.BOTH.,#13140);
#13140=SURFACE_SIDE_STYLE('',(#13153));
#13153=SURFACE_STYLE_FILL_AREA(#13166);
#13166=FILL_AREA_STYLE('Hex nut M4 finish',(#13179));
#13179=FILL_AREA_STYLE_COLOUR('Hex nut M4 finish',#13192);
#13192=COLOUR_RGB('Hex nut M4 finish',0.607843137254902,0.647058823529412,
0.701960784313725);
ENDSEC;
END-ISO-10303-21;
